ISO-10303-21;
HEADER;
/* Generated by software containing ST-Developer
 * from STEP Tools, Inc. (www.steptools.com) 
 */

FILE_DESCRIPTION(
/* description */ (''),
/* implementation_level */ '2;1');

FILE_NAME(
/* name */ 'Top_Plate.step',
/* time_stamp */ '2026-10-22T13:39:42+06:00',
/* author */ (''),
/* organization */ (''),
/* preprocessor_version */ 'ST-DEVELOPER v20.2',
/* originating_system */ 'Autodesk Translation Framework v15.15.0.0',
/* authorisation */ '');

FILE_SCHEMA (('AUTOMOTIVE_DESIGN { 1 0 10303 214 3 1 1 }'));
ENDSEC;

DATA;
#10=MECHANICAL_DESIGN_GEOMETRIC_PRESENTATION_REPRESENTATION('',(#310),#17836);
#149=SPHERICAL_SURFACE('',#10181,0.499999999999998);
#150=SPHERICAL_SURFACE('',#10185,0.499999999999998);
#151=SPHERICAL_SURFACE('',#10190,0.5);
#152=SPHERICAL_SURFACE('',#10196,0.499999999999998);
#153=SPHERICAL_SURFACE('',#10206,0.500000000000007);
#154=SPHERICAL_SURFACE('',#10215,0.500000000000007);
#155=SPHERICAL_SURFACE('',#10228,0.5);
#156=SPHERICAL_SURFACE('',#10232,0.5);
#157=SPHERICAL_SURFACE('',#10237,0.5);
#158=SPHERICAL_SURFACE('',#10243,0.5);
#159=SPHERICAL_SURFACE('',#10252,0.500000000000007);
#160=SPHERICAL_SURFACE('',#10260,0.500000000000007);
#161=SPHERICAL_SURFACE('',#10265,0.500000000000007);
#162=SPHERICAL_SURFACE('',#10271,0.499999999999998);
#227=TOROIDAL_SURFACE('',#10173,0.999999999999996,0.500000000000007);
#228=TOROIDAL_SURFACE('',#10177,1.,0.500000000000007);
#229=TOROIDAL_SURFACE('',#10202,0.999999999999996,0.500000000000007);
#230=TOROIDAL_SURFACE('',#10209,1.,0.500000000000007);
#231=TOROIDAL_SURFACE('',#10218,1.,0.500000000000007);
#232=TOROIDAL_SURFACE('',#10222,1.,0.500000000000007);
#233=TOROIDAL_SURFACE('',#10248,0.99999999999999,0.500000000000007);
#234=TOROIDAL_SURFACE('',#10256,0.999999999999994,0.5);
#269=ELLIPSE('',#10142,0.707106781186543,0.5);
#270=ELLIPSE('',#10148,0.707106781186553,0.5);
#290=SHAPE_REPRESENTATION_RELATIONSHIP('SRR','None',#17877,#300);
#300=ADVANCED_BREP_SHAPE_REPRESENTATION('',(#320),#17829);
#310=STYLED_ITEM('',(#17959),#320);
#320=MANIFOLD_SOLID_BREP('Top_Plate',#9631);
#408=CYLINDRICAL_SURFACE('',#10102,4.);
#409=CYLINDRICAL_SURFACE('',#10106,4.);
#410=CYLINDRICAL_SURFACE('',#10110,4.);
#411=CYLINDRICAL_SURFACE('',#10114,4.);
#412=CYLINDRICAL_SURFACE('',#10118,4.);
#413=CYLINDRICAL_SURFACE('',#10122,4.);
#414=CYLINDRICAL_SURFACE('',#10126,4.);
#415=CYLINDRICAL_SURFACE('',#10130,4.);
#416=CYLINDRICAL_SURFACE('',#10141,0.5);
#417=CYLINDRICAL_SURFACE('',#10143,0.5);
#418=CYLINDRICAL_SURFACE('',#10147,0.5);
#419=CYLINDRICAL_SURFACE('',#10149,0.5);
#420=CYLINDRICAL_SURFACE('',#10163,0.5);
#421=CYLINDRICAL_SURFACE('',#10171,0.5);
#422=CYLINDRICAL_SURFACE('',#10189,0.5);
#423=CYLINDRICAL_SURFACE('',#10194,0.5);
#424=CYLINDRICAL_SURFACE('',#10195,0.5);
#425=CYLINDRICAL_SURFACE('',#10200,0.5);
#426=CYLINDRICAL_SURFACE('',#10201,0.5);
#427=CYLINDRICAL_SURFACE('',#10213,0.5);
#428=CYLINDRICAL_SURFACE('',#10214,0.5);
#429=CYLINDRICAL_SURFACE('',#10226,0.5);
#430=CYLINDRICAL_SURFACE('',#10227,0.5);
#431=CYLINDRICAL_SURFACE('',#10236,0.5);
#432=CYLINDRICAL_SURFACE('',#10241,0.5);
#433=CYLINDRICAL_SURFACE('',#10242,0.5);
#434=CYLINDRICAL_SURFACE('',#10246,0.5);
#435=CYLINDRICAL_SURFACE('',#10247,0.5);
#436=CYLINDRICAL_SURFACE('',#10255,0.5);
#437=CYLINDRICAL_SURFACE('',#10264,0.5);
#438=CYLINDRICAL_SURFACE('',#10269,0.5);
#439=CYLINDRICAL_SURFACE('',#10270,0.5);
#440=CYLINDRICAL_SURFACE('',#10275,0.5);
#441=CYLINDRICAL_SURFACE('',#10276,0.5);
#442=CYLINDRICAL_SURFACE('',#10277,0.5);
#443=CYLINDRICAL_SURFACE('',#10278,0.5);
#444=CYLINDRICAL_SURFACE('',#10279,0.5);
#445=CYLINDRICAL_SURFACE('',#10280,0.5);
#446=CYLINDRICAL_SURFACE('',#10281,0.5);
#447=CYLINDRICAL_SURFACE('',#10282,0.5);
#448=CYLINDRICAL_SURFACE('',#10283,0.5);
#449=CYLINDRICAL_SURFACE('',#10284,0.5);
#450=CYLINDRICAL_SURFACE('',#10285,0.5);
#451=CYLINDRICAL_SURFACE('',#10286,0.5);
#452=CYLINDRICAL_SURFACE('',#10287,0.5);
#453=CYLINDRICAL_SURFACE('',#10288,0.5);
#454=CYLINDRICAL_SURFACE('',#10289,0.5);
#819=LINE('',#14995,#1484);
#820=LINE('',#15002,#1485);
#821=LINE('',#15009,#1486);
#822=LINE('',#15016,#1487);
#823=LINE('',#15023,#1488);
#824=LINE('',#15030,#1489);
#825=LINE('',#15037,#1490);
#826=LINE('',#15044,#1491);
#827=LINE('',#15052,#1492);
#828=LINE('',#15054,#1493);
#829=LINE('',#15056,#1494);
#830=LINE('',#15059,#1495);
#831=LINE('',#15065,#1496);
#832=LINE('',#15069,#1497);
#833=LINE('',#15071,#1498);
#834=LINE('',#15072,#1499);
#835=LINE('',#15074,#1500);
#836=LINE('',#15075,#1501);
#837=LINE('',#15078,#1502);
#838=LINE('',#15081,#1503);
#839=LINE('',#15084,#1504);
#840=LINE('',#15087,#1505);
#841=LINE('',#15090,#1506);
#842=LINE('',#15091,#1507);
#843=LINE('',#15094,#1508);
#844=LINE('',#15095,#1509);
#845=LINE('',#15099,#1510);
#846=LINE('',#15102,#1511);
#847=LINE('',#15106,#1512);
#848=LINE('',#15108,#1513);
#849=LINE('',#15110,#1514);
#850=LINE('',#15112,#1515);
#851=LINE('',#15114,#1516);
#852=LINE('',#15116,#1517);
#853=LINE('',#15118,#1518);
#854=LINE('',#15120,#1519);
#855=LINE('',#15124,#1520);
#856=LINE('',#15126,#1521);
#857=LINE('',#15130,#1522);
#858=LINE('',#15134,#1523);
#859=LINE('',#15136,#1524);
#860=LINE('',#15140,#1525);
#861=LINE('',#15141,#1526);
#862=LINE('',#15146,#1527);
#863=LINE('',#15148,#1528);
#864=LINE('',#15151,#1529);
#865=LINE('',#15156,#1530);
#866=LINE('',#15160,#1531);
#867=LINE('',#15161,#1532);
#868=LINE('',#15163,#1533);
#869=LINE('',#15166,#1534);
#870=LINE('',#15170,#1535);
#871=LINE('',#15172,#1536);
#872=LINE('',#15176,#1537);
#873=LINE('',#15178,#1538);
#874=LINE('',#15182,#1539);
#875=LINE('',#15186,#1540);
#876=LINE('',#15188,#1541);
#877=LINE('',#15192,#1542);
#878=LINE('',#15194,#1543);
#879=LINE('',#15195,#1544);
#880=LINE('',#15197,#1545);
#881=LINE('',#15198,#1546);
#882=LINE('',#15201,#1547);
#883=LINE('',#15202,#1548);
#884=LINE('',#15205,#1549);
#885=LINE('',#15232,#1550);
#886=LINE('',#15240,#1551);
#887=LINE('',#15242,#1552);
#888=LINE('',#15243,#1553);
#889=LINE('',#15251,#1554);
#890=LINE('',#15252,#1555);
#891=LINE('',#15254,#1556);
#892=LINE('',#15272,#1557);
#893=LINE('',#15274,#1558);
#894=LINE('',#15275,#1559);
#895=LINE('',#15293,#1560);
#896=LINE('',#15295,#1561);
#897=LINE('',#15296,#1562);
#898=LINE('',#15310,#1563);
#899=LINE('',#15318,#1564);
#900=LINE('',#15320,#1565);
#901=LINE('',#15321,#1566);
#902=LINE('',#15327,#1567);
#903=LINE('',#15328,#1568);
#904=LINE('',#15330,#1569);
#905=LINE('',#15342,#1570);
#906=LINE('',#15362,#1571);
#907=LINE('',#15364,#1572);
#908=LINE('',#15372,#1573);
#909=LINE('',#15373,#1574);
#910=LINE('',#15375,#1575);
#911=LINE('',#15377,#1576);
#912=LINE('',#15379,#1577);
#913=LINE('',#15381,#1578);
#914=LINE('',#15383,#1579);
#915=LINE('',#15384,#1580);
#916=LINE('',#15386,#1581);
#917=LINE('',#15388,#1582);
#918=LINE('',#15390,#1583);
#919=LINE('',#15392,#1584);
#920=LINE('',#15394,#1585);
#921=LINE('',#15396,#1586);
#922=LINE('',#15398,#1587);
#923=LINE('',#15400,#1588);
#924=LINE('',#15402,#1589);
#925=LINE('',#15403,#1590);
#1484=VECTOR('',#11921,4.);
#1485=VECTOR('',#11930,4.);
#1486=VECTOR('',#11939,4.);
#1487=VECTOR('',#11948,4.);
#1488=VECTOR('',#11957,4.);
#1489=VECTOR('',#11966,4.);
#1490=VECTOR('',#11975,4.);
#1491=VECTOR('',#11984,4.);
#1492=VECTOR('',#11993,10.);
#1493=VECTOR('',#11994,10.);
#1494=VECTOR('',#11995,10.);
#1495=VECTOR('',#11998,10.);
#1496=VECTOR('',#12003,10.);
#1497=VECTOR('',#12006,10.);
#1498=VECTOR('',#12007,10.);
#1499=VECTOR('',#12008,10.);
#1500=VECTOR('',#12011,10.);
#1501=VECTOR('',#12012,10.);
#1502=VECTOR('',#12015,10.);
#1503=VECTOR('',#12018,10.);
#1504=VECTOR('',#12021,10.);
#1505=VECTOR('',#12024,10.);
#1506=VECTOR('',#12027,10.);
#1507=VECTOR('',#12028,10.);
#1508=VECTOR('',#12031,10.);
#1509=VECTOR('',#12032,10.);
#1510=VECTOR('',#12037,10.);
#1511=VECTOR('',#12040,10.);
#1512=VECTOR('',#12045,10.);
#1513=VECTOR('',#12046,10.);
#1514=VECTOR('',#12047,10.);
#1515=VECTOR('',#12048,10.);
#1516=VECTOR('',#12049,10.);
#1517=VECTOR('',#12050,10.);
#1518=VECTOR('',#12051,10.);
#1519=VECTOR('',#12052,10.);
#1520=VECTOR('',#12055,10.);
#1521=VECTOR('',#12056,10.);
#1522=VECTOR('',#12059,10.);
#1523=VECTOR('',#12062,10.);
#1524=VECTOR('',#12063,10.);
#1525=VECTOR('',#12066,10.);
#1526=VECTOR('',#12067,10.);
#1527=VECTOR('',#12072,10.);
#1528=VECTOR('',#12073,10.);
#1529=VECTOR('',#12076,10.);
#1530=VECTOR('',#12081,10.);
#1531=VECTOR('',#12084,10.);
#1532=VECTOR('',#12085,10.);
#1533=VECTOR('',#12088,10.);
#1534=VECTOR('',#12091,10.);
#1535=VECTOR('',#12096,10.);
#1536=VECTOR('',#12097,10.);
#1537=VECTOR('',#12100,10.);
#1538=VECTOR('',#12101,10.);
#1539=VECTOR('',#12104,10.);
#1540=VECTOR('',#12107,10.);
#1541=VECTOR('',#12108,10.);
#1542=VECTOR('',#12111,10.);
#1543=VECTOR('',#12112,10.);
#1544=VECTOR('',#12113,10.);
#1545=VECTOR('',#12114,10.);
#1546=VECTOR('',#12115,10.);
#1547=VECTOR('',#12118,10.);
#1548=VECTOR('',#12119,10.);
#1549=VECTOR('',#12122,10.);
#1550=VECTOR('',#12159,10.);
#1551=VECTOR('',#12170,10.);
#1552=VECTOR('',#12173,10.);
#1553=VECTOR('',#12174,10.);
#1554=VECTOR('',#12185,10.);
#1555=VECTOR('',#12186,10.);
#1556=VECTOR('',#12189,10.);
#1557=VECTOR('',#12214,10.);
#1558=VECTOR('',#12217,10.);
#1559=VECTOR('',#12218,10.);
#1560=VECTOR('',#12243,10.);
#1561=VECTOR('',#12246,10.);
#1562=VECTOR('',#12247,10.);
#1563=VECTOR('',#12266,10.);
#1564=VECTOR('',#12277,10.);
#1565=VECTOR('',#12280,10.);
#1566=VECTOR('',#12281,10.);
#1567=VECTOR('',#12290,10.);
#1568=VECTOR('',#12291,10.);
#1569=VECTOR('',#12294,10.);
#1570=VECTOR('',#12311,10.);
#1571=VECTOR('',#12340,10.);
#1572=VECTOR('',#12343,10.);
#1573=VECTOR('',#12354,10.);
#1574=VECTOR('',#12355,10.);
#1575=VECTOR('',#12358,10.);
#1576=VECTOR('',#12361,10.);
#1577=VECTOR('',#12364,10.);
#1578=VECTOR('',#12367,10.);
#1579=VECTOR('',#12370,10.);
#1580=VECTOR('',#12371,10.);
#1581=VECTOR('',#12374,10.);
#1582=VECTOR('',#12377,10.);
#1583=VECTOR('',#12380,10.);
#1584=VECTOR('',#12383,10.);
#1585=VECTOR('',#12386,10.);
#1586=VECTOR('',#12389,10.);
#1587=VECTOR('',#12392,10.);
#1588=VECTOR('',#12395,10.);
#1589=VECTOR('',#12398,10.);
#1590=VECTOR('',#12399,10.);
#1981=FACE_BOUND('',#2841,.T.);
#1982=FACE_BOUND('',#2842,.T.);
#1983=FACE_BOUND('',#2843,.T.);
#1984=FACE_BOUND('',#2844,.T.);
#1985=FACE_BOUND('',#2854,.T.);
#1986=FACE_BOUND('',#2855,.T.);
#1987=FACE_BOUND('',#2856,.T.);
#1988=FACE_BOUND('',#2857,.T.);
#2197=FACE_OUTER_BOUND('',#2818,.T.);
#2198=FACE_OUTER_BOUND('',#2819,.T.);
#2199=FACE_OUTER_BOUND('',#2820,.T.);
#2200=FACE_OUTER_BOUND('',#2821,.T.);
#2201=FACE_OUTER_BOUND('',#2822,.T.);
#2202=FACE_OUTER_BOUND('',#2823,.T.);
#2203=FACE_OUTER_BOUND('',#2824,.T.);
#2204=FACE_OUTER_BOUND('',#2825,.T.);
#2205=FACE_OUTER_BOUND('',#2826,.T.);
#2206=FACE_OUTER_BOUND('',#2827,.T.);
#2207=FACE_OUTER_BOUND('',#2828,.T.);
#2208=FACE_OUTER_BOUND('',#2829,.T.);
#2209=FACE_OUTER_BOUND('',#2830,.T.);
#2210=FACE_OUTER_BOUND('',#2831,.T.);
#2211=FACE_OUTER_BOUND('',#2832,.T.);
#2212=FACE_OUTER_BOUND('',#2833,.T.);
#2213=FACE_OUTER_BOUND('',#2834,.T.);
#2214=FACE_OUTER_BOUND('',#2835,.T.);
#2215=FACE_OUTER_BOUND('',#2836,.T.);
#2216=FACE_OUTER_BOUND('',#2837,.T.);
#2217=FACE_OUTER_BOUND('',#2838,.T.);
#2218=FACE_OUTER_BOUND('',#2839,.T.);
#2219=FACE_OUTER_BOUND('',#2840,.T.);
#2220=FACE_OUTER_BOUND('',#2845,.T.);
#2221=FACE_OUTER_BOUND('',#2846,.T.);
#2222=FACE_OUTER_BOUND('',#2847,.T.);
#2223=FACE_OUTER_BOUND('',#2848,.T.);
#2224=FACE_OUTER_BOUND('',#2849,.T.);
#2225=FACE_OUTER_BOUND('',#2850,.T.);
#2226=FACE_OUTER_BOUND('',#2851,.T.);
#2227=FACE_OUTER_BOUND('',#2852,.T.);
#2228=FACE_OUTER_BOUND('',#2853,.T.);
#2229=FACE_OUTER_BOUND('',#2858,.T.);
#2230=FACE_OUTER_BOUND('',#2859,.T.);
#2231=FACE_OUTER_BOUND('',#2860,.T.);
#2232=FACE_OUTER_BOUND('',#2861,.T.);
#2233=FACE_OUTER_BOUND('',#2862,.T.);
#2234=FACE_OUTER_BOUND('',#2863,.T.);
#2235=FACE_OUTER_BOUND('',#2864,.T.);
#2236=FACE_OUTER_BOUND('',#2865,.T.);
#2237=FACE_OUTER_BOUND('',#2866,.T.);
#2238=FACE_OUTER_BOUND('',#2867,.T.);
#2239=FACE_OUTER_BOUND('',#2868,.T.);
#2240=FACE_OUTER_BOUND('',#2869,.T.);
#2241=FACE_OUTER_BOUND('',#2870,.T.);
#2242=FACE_OUTER_BOUND('',#2871,.T.);
#2243=FACE_OUTER_BOUND('',#2872,.T.);
#2244=FACE_OUTER_BOUND('',#2873,.T.);
#2245=FACE_OUTER_BOUND('',#2874,.T.);
#2246=FACE_OUTER_BOUND('',#2875,.T.);
#2247=FACE_OUTER_BOUND('',#2876,.T.);
#2248=FACE_OUTER_BOUND('',#2877,.T.);
#2249=FACE_OUTER_BOUND('',#2878,.T.);
#2250=FACE_OUTER_BOUND('',#2879,.T.);
#2251=FACE_OUTER_BOUND('',#2880,.T.);
#2252=FACE_OUTER_BOUND('',#2881,.T.);
#2253=FACE_OUTER_BOUND('',#2882,.T.);
#2254=FACE_OUTER_BOUND('',#2883,.T.);
#2255=FACE_OUTER_BOUND('',#2884,.T.);
#2256=FACE_OUTER_BOUND('',#2885,.T.);
#2257=FACE_OUTER_BOUND('',#2886,.T.);
#2258=FACE_OUTER_BOUND('',#2887,.T.);
#2259=FACE_OUTER_BOUND('',#2888,.T.);
#2260=FACE_OUTER_BOUND('',#2889,.T.);
#2261=FACE_OUTER_BOUND('',#2890,.T.);
#2262=FACE_OUTER_BOUND('',#2891,.T.);
#2263=FACE_OUTER_BOUND('',#2892,.T.);
#2264=FACE_OUTER_BOUND('',#2893,.T.);
#2265=FACE_OUTER_BOUND('',#2894,.T.);
#2266=FACE_OUTER_BOUND('',#2895,.T.);
#2267=FACE_OUTER_BOUND('',#2896,.T.);
#2268=FACE_OUTER_BOUND('',#2897,.T.);
#2269=FACE_OUTER_BOUND('',#2898,.T.);
#2270=FACE_OUTER_BOUND('',#2899,.T.);
#2271=FACE_OUTER_BOUND('',#2900,.T.);
#2272=FACE_OUTER_BOUND('',#2901,.T.);
#2273=FACE_OUTER_BOUND('',#2902,.T.);
#2274=FACE_OUTER_BOUND('',#2903,.T.);
#2275=FACE_OUTER_BOUND('',#2904,.T.);
#2276=FACE_OUTER_BOUND('',#2905,.T.);
#2277=FACE_OUTER_BOUND('',#2906,.T.);
#2278=FACE_OUTER_BOUND('',#2907,.T.);
#2279=FACE_OUTER_BOUND('',#2908,.T.);
#2280=FACE_OUTER_BOUND('',#2909,.T.);
#2281=FACE_OUTER_BOUND('',#2910,.T.);
#2282=FACE_OUTER_BOUND('',#2911,.T.);
#2283=FACE_OUTER_BOUND('',#2912,.T.);
#2284=FACE_OUTER_BOUND('',#2913,.T.);
#2285=FACE_OUTER_BOUND('',#2914,.T.);
#2286=FACE_OUTER_BOUND('',#2915,.T.);
#2287=FACE_OUTER_BOUND('',#2916,.T.);
#2288=FACE_OUTER_BOUND('',#2917,.T.);
#2289=FACE_OUTER_BOUND('',#2918,.T.);
#2290=FACE_OUTER_BOUND('',#2919,.T.);
#2291=FACE_OUTER_BOUND('',#2920,.T.);
#2292=FACE_OUTER_BOUND('',#2921,.T.);
#2293=FACE_OUTER_BOUND('',#2922,.T.);
#2294=FACE_OUTER_BOUND('',#2923,.T.);
#2295=FACE_OUTER_BOUND('',#2924,.T.);
#2818=EDGE_LOOP('',(#6817,#6818,#6819,#6820));
#2819=EDGE_LOOP('',(#6821));
#2820=EDGE_LOOP('',(#6822,#6823,#6824,#6825));
#2821=EDGE_LOOP('',(#6826));
#2822=EDGE_LOOP('',(#6827,#6828,#6829,#6830));
#2823=EDGE_LOOP('',(#6831));
#2824=EDGE_LOOP('',(#6832,#6833,#6834,#6835));
#2825=EDGE_LOOP('',(#6836));
#2826=EDGE_LOOP('',(#6837,#6838,#6839,#6840));
#2827=EDGE_LOOP('',(#6841));
#2828=EDGE_LOOP('',(#6842,#6843,#6844,#6845));
#2829=EDGE_LOOP('',(#6846));
#2830=EDGE_LOOP('',(#6847,#6848,#6849,#6850));
#2831=EDGE_LOOP('',(#6851));
#2832=EDGE_LOOP('',(#6852,#6853,#6854,#6855));
#2833=EDGE_LOOP('',(#6856));
#2834=EDGE_LOOP('',(#6857,#6858,#6859,#6860,#6861,#6862));
#2835=EDGE_LOOP('',(#6863,#6864,#6865,#6866,#6867,#6868));
#2836=EDGE_LOOP('',(#6869,#6870,#6871,#6872));
#2837=EDGE_LOOP('',(#6873,#6874,#6875,#6876));
#2838=EDGE_LOOP('',(#6877,#6878,#6879,#6880));
#2839=EDGE_LOOP('',(#6881,#6882,#6883,#6884));
#2840=EDGE_LOOP('',(#6885,#6886,#6887,#6888));
#2841=EDGE_LOOP('',(#6889));
#2842=EDGE_LOOP('',(#6890));
#2843=EDGE_LOOP('',(#6891));
#2844=EDGE_LOOP('',(#6892));
#2845=EDGE_LOOP('',(#6893,#6894,#6895,#6896));
#2846=EDGE_LOOP('',(#6897,#6898,#6899,#6900));
#2847=EDGE_LOOP('',(#6901,#6902,#6903,#6904,#6905,#6906,#6907,#6908,#6909,
#6910,#6911,#6912,#6913,#6914,#6915,#6916,#6917,#6918,#6919,#6920,#6921,
#6922,#6923,#6924));
#2848=EDGE_LOOP('',(#6925,#6926,#6927,#6928,#6929,#6930));
#2849=EDGE_LOOP('',(#6931,#6932,#6933,#6934,#6935,#6936));
#2850=EDGE_LOOP('',(#6937,#6938,#6939,#6940));
#2851=EDGE_LOOP('',(#6941,#6942,#6943,#6944));
#2852=EDGE_LOOP('',(#6945,#6946,#6947,#6948,#6949,#6950,#6951,#6952,#6953,
#6954,#6955,#6956,#6957,#6958,#6959,#6960,#6961,#6962,#6963,#6964,#6965,
#6966,#6967,#6968));
#2853=EDGE_LOOP('',(#6969,#6970,#6971,#6972));
#2854=EDGE_LOOP('',(#6973));
#2855=EDGE_LOOP('',(#6974));
#2856=EDGE_LOOP('',(#6975));
#2857=EDGE_LOOP('',(#6976));
#2858=EDGE_LOOP('',(#6977,#6978,#6979,#6980));
#2859=EDGE_LOOP('',(#6981,#6982,#6983,#6984));
#2860=EDGE_LOOP('',(#6985,#6986,#6987,#6988));
#2861=EDGE_LOOP('',(#6989,#6990,#6991));
#2862=EDGE_LOOP('',(#6992,#6993,#6994));
#2863=EDGE_LOOP('',(#6995,#6996,#6997,#6998));
#2864=EDGE_LOOP('',(#6999,#7000,#7001));
#2865=EDGE_LOOP('',(#7002,#7003,#7004,#7005));
#2866=EDGE_LOOP('',(#7006,#7007,#7008,#7009));
#2867=EDGE_LOOP('',(#7010,#7011,#7012));
#2868=EDGE_LOOP('',(#7013,#7014,#7015,#7016));
#2869=EDGE_LOOP('',(#7017,#7018,#7019,#7020));
#2870=EDGE_LOOP('',(#7021,#7022,#7023,#7024));
#2871=EDGE_LOOP('',(#7025,#7026,#7027));
#2872=EDGE_LOOP('',(#7028,#7029,#7030,#7031));
#2873=EDGE_LOOP('',(#7032,#7033,#7034,#7035));
#2874=EDGE_LOOP('',(#7036,#7037,#7038,#7039));
#2875=EDGE_LOOP('',(#7040,#7041,#7042));
#2876=EDGE_LOOP('',(#7043,#7044,#7045,#7046));
#2877=EDGE_LOOP('',(#7047,#7048,#7049,#7050));
#2878=EDGE_LOOP('',(#7051,#7052,#7053,#7054));
#2879=EDGE_LOOP('',(#7055,#7056,#7057,#7058));
#2880=EDGE_LOOP('',(#7059,#7060,#7061));
#2881=EDGE_LOOP('',(#7062,#7063,#7064));
#2882=EDGE_LOOP('',(#7065,#7066,#7067,#7068));
#2883=EDGE_LOOP('',(#7069,#7070,#7071));
#2884=EDGE_LOOP('',(#7072,#7073,#7074,#7075));
#2885=EDGE_LOOP('',(#7076,#7077,#7078,#7079));
#2886=EDGE_LOOP('',(#7080,#7081,#7082));
#2887=EDGE_LOOP('',(#7083,#7084,#7085,#7086));
#2888=EDGE_LOOP('',(#7087,#7088,#7089,#7090));
#2889=EDGE_LOOP('',(#7091,#7092,#7093,#7094));
#2890=EDGE_LOOP('',(#7095,#7096,#7097));
#2891=EDGE_LOOP('',(#7098,#7099,#7100,#7101));
#2892=EDGE_LOOP('',(#7102,#7103,#7104,#7105));
#2893=EDGE_LOOP('',(#7106,#7107,#7108));
#2894=EDGE_LOOP('',(#7109,#7110,#7111,#7112));
#2895=EDGE_LOOP('',(#7113,#7114,#7115));
#2896=EDGE_LOOP('',(#7116,#7117,#7118,#7119));
#2897=EDGE_LOOP('',(#7120,#7121,#7122,#7123));
#2898=EDGE_LOOP('',(#7124,#7125,#7126));
#2899=EDGE_LOOP('',(#7127,#7128,#7129,#7130));
#2900=EDGE_LOOP('',(#7131,#7132,#7133,#7134));
#2901=EDGE_LOOP('',(#7135,#7136,#7137,#7138));
#2902=EDGE_LOOP('',(#7139,#7140,#7141,#7142));
#2903=EDGE_LOOP('',(#7143,#7144,#7145,#7146));
#2904=EDGE_LOOP('',(#7147,#7148,#7149,#7150));
#2905=EDGE_LOOP('',(#7151,#7152,#7153,#7154));
#2906=EDGE_LOOP('',(#7155,#7156,#7157,#7158));
#2907=EDGE_LOOP('',(#7159,#7160,#7161,#7162));
#2908=EDGE_LOOP('',(#7163,#7164,#7165,#7166));
#2909=EDGE_LOOP('',(#7167,#7168,#7169,#7170));
#2910=EDGE_LOOP('',(#7171,#7172,#7173,#7174));
#2911=EDGE_LOOP('',(#7175,#7176,#7177,#7178));
#2912=EDGE_LOOP('',(#7179,#7180,#7181,#7182));
#2913=EDGE_LOOP('',(#7183,#7184,#7185,#7186));
#2914=EDGE_LOOP('',(#7187,#7188,#7189,#7190));
#2915=EDGE_LOOP('',(#7191,#7192,#7193,#7194));
#2916=EDGE_LOOP('',(#7195,#7196,#7197,#7198));
#2917=EDGE_LOOP('',(#7199,#7200,#7201,#7202));
#2918=EDGE_LOOP('',(#7203,#7204,#7205,#7206));
#2919=EDGE_LOOP('',(#7207,#7208,#7209,#7210));
#2920=EDGE_LOOP('',(#7211,#7212,#7213,#7214));
#2921=EDGE_LOOP('',(#7215,#7216,#7217,#7218));
#2922=EDGE_LOOP('',(#7219,#7220,#7221,#7222));
#2923=EDGE_LOOP('',(#7223,#7224,#7225,#7226));
#2924=EDGE_LOOP('',(#7227,#7228,#7229,#7230));
#3484=CIRCLE('',#10103,4.);
#3485=CIRCLE('',#10104,4.);
#3486=CIRCLE('',#10107,4.);
#3487=CIRCLE('',#10108,4.);
#3488=CIRCLE('',#10111,4.);
#3489=CIRCLE('',#10112,4.);
#3490=CIRCLE('',#10115,4.);
#3491=CIRCLE('',#10116,4.);
#3492=CIRCLE('',#10119,4.);
#3493=CIRCLE('',#10120,4.);
#3494=CIRCLE('',#10123,4.);
#3495=CIRCLE('',#10124,4.);
#3496=CIRCLE('',#10127,4.);
#3497=CIRCLE('',#10128,4.);
#3498=CIRCLE('',#10131,4.);
#3499=CIRCLE('',#10132,4.);
#3500=CIRCLE('',#10135,0.5);
#3501=CIRCLE('',#10136,0.5);
#3502=CIRCLE('',#10138,0.5);
#3503=CIRCLE('',#10139,0.5);
#3504=CIRCLE('',#10144,0.500000000000007);
#3505=CIRCLE('',#10150,0.500000000000007);
#3506=CIRCLE('',#10152,0.999999999999972);
#3507=CIRCLE('',#10153,1.);
#3508=CIRCLE('',#10154,0.999999999999997);
#3509=CIRCLE('',#10155,0.999999999999996);
#3510=CIRCLE('',#10157,0.5);
#3511=CIRCLE('',#10158,0.5);
#3512=CIRCLE('',#10160,0.5);
#3513=CIRCLE('',#10161,0.5);
#3514=CIRCLE('',#10164,0.500000000000007);
#3515=CIRCLE('',#10166,1.);
#3516=CIRCLE('',#10167,1.);
#3517=CIRCLE('',#10168,1.);
#3518=CIRCLE('',#10169,0.999999999999992);
#3519=CIRCLE('',#10172,0.500000000000007);
#3520=CIRCLE('',#10174,0.5);
#3521=CIRCLE('',#10175,0.499999999999998);
#3522=CIRCLE('',#10176,0.500000000000007);
#3523=CIRCLE('',#10178,0.500000000000007);
#3524=CIRCLE('',#10179,0.5);
#3525=CIRCLE('',#10180,0.500000000000007);
#3526=CIRCLE('',#10182,0.500000000000007);
#3527=CIRCLE('',#10183,0.499999999999998);
#3528=CIRCLE('',#10184,0.5);
#3529=CIRCLE('',#10186,0.500000000000007);
#3530=CIRCLE('',#10187,0.499999999999998);
#3531=CIRCLE('',#10188,0.499999999999998);
#3532=CIRCLE('',#10191,0.500000000000007);
#3533=CIRCLE('',#10192,0.5);
#3534=CIRCLE('',#10193,0.499999999999998);
#3535=CIRCLE('',#10197,0.5);
#3536=CIRCLE('',#10198,0.499999999999998);
#3537=CIRCLE('',#10199,0.500000000000007);
#3538=CIRCLE('',#10203,0.5);
#3539=CIRCLE('',#10204,0.499999999999998);
#3540=CIRCLE('',#10205,0.500000000000007);
#3541=CIRCLE('',#10207,0.499999999999998);
#3542=CIRCLE('',#10208,0.5);
#3543=CIRCLE('',#10210,0.499999999999998);
#3544=CIRCLE('',#10211,0.5);
#3545=CIRCLE('',#10212,0.500000000000007);
#3546=CIRCLE('',#10216,0.500000000000007);
#3547=CIRCLE('',#10217,0.5);
#3548=CIRCLE('',#10219,0.500000000000005);
#3549=CIRCLE('',#10220,0.5);
#3550=CIRCLE('',#10221,0.500000000000007);
#3551=CIRCLE('',#10223,0.5);
#3552=CIRCLE('',#10224,0.5);
#3553=CIRCLE('',#10225,0.500000000000007);
#3554=CIRCLE('',#10229,0.500000000000007);
#3555=CIRCLE('',#10230,0.5);
#3556=CIRCLE('',#10231,0.499999999999998);
#3557=CIRCLE('',#10233,0.500000000000007);
#3558=CIRCLE('',#10234,0.5);
#3559=CIRCLE('',#10235,0.499999999999998);
#3560=CIRCLE('',#10238,0.500000000000007);
#3561=CIRCLE('',#10239,0.5);
#3562=CIRCLE('',#10240,0.5);
#3563=CIRCLE('',#10244,0.5);
#3564=CIRCLE('',#10245,0.500000000000007);
#3565=CIRCLE('',#10249,0.499999999999999);
#3566=CIRCLE('',#10250,0.499999999999998);
#3567=CIRCLE('',#10251,0.500000000000007);
#3568=CIRCLE('',#10253,0.500000000000007);
#3569=CIRCLE('',#10254,0.5);
#3570=CIRCLE('',#10257,0.5);
#3571=CIRCLE('',#10258,0.499999999999999);
#3572=CIRCLE('',#10259,0.500000000000007);
#3573=CIRCLE('',#10261,0.499999999999998);
#3574=CIRCLE('',#10262,0.500000000000007);
#3575=CIRCLE('',#10263,0.5);
#3576=CIRCLE('',#10266,0.499999999999999);
#3577=CIRCLE('',#10267,0.500000000000007);
#3578=CIRCLE('',#10268,0.5);
#3579=CIRCLE('',#10272,0.499999999999999);
#3580=CIRCLE('',#10273,0.499999999999998);
#3581=CIRCLE('',#10274,0.500000000000007);
#4132=VERTEX_POINT('',#14992);
#4133=VERTEX_POINT('',#14994);
#4134=VERTEX_POINT('',#14999);
#4135=VERTEX_POINT('',#15001);
#4136=VERTEX_POINT('',#15006);
#4137=VERTEX_POINT('',#15008);
#4138=VERTEX_POINT('',#15013);
#4139=VERTEX_POINT('',#15015);
#4140=VERTEX_POINT('',#15020);
#4141=VERTEX_POINT('',#15022);
#4142=VERTEX_POINT('',#15027);
#4143=VERTEX_POINT('',#15029);
#4144=VERTEX_POINT('',#15034);
#4145=VERTEX_POINT('',#15036);
#4146=VERTEX_POINT('',#15041);
#4147=VERTEX_POINT('',#15043);
#4148=VERTEX_POINT('',#15048);
#4149=VERTEX_POINT('',#15049);
#4150=VERTEX_POINT('',#15051);
#4151=VERTEX_POINT('',#15053);
#4152=VERTEX_POINT('',#15055);
#4153=VERTEX_POINT('',#15057);
#4154=VERTEX_POINT('',#15061);
#4155=VERTEX_POINT('',#15062);
#4156=VERTEX_POINT('',#15064);
#4157=VERTEX_POINT('',#15066);
#4158=VERTEX_POINT('',#15068);
#4159=VERTEX_POINT('',#15070);
#4160=VERTEX_POINT('',#15077);
#4161=VERTEX_POINT('',#15079);
#4162=VERTEX_POINT('',#15083);
#4163=VERTEX_POINT('',#15085);
#4164=VERTEX_POINT('',#15089);
#4165=VERTEX_POINT('',#15093);
#4166=VERTEX_POINT('',#15097);
#4167=VERTEX_POINT('',#15101);
#4168=VERTEX_POINT('',#15105);
#4169=VERTEX_POINT('',#15107);
#4170=VERTEX_POINT('',#15109);
#4171=VERTEX_POINT('',#15111);
#4172=VERTEX_POINT('',#15113);
#4173=VERTEX_POINT('',#15115);
#4174=VERTEX_POINT('',#15117);
#4175=VERTEX_POINT('',#15119);
#4176=VERTEX_POINT('',#15121);
#4177=VERTEX_POINT('',#15123);
#4178=VERTEX_POINT('',#15125);
#4179=VERTEX_POINT('',#15127);
#4180=VERTEX_POINT('',#15129);
#4181=VERTEX_POINT('',#15131);
#4182=VERTEX_POINT('',#15133);
#4183=VERTEX_POINT('',#15135);
#4184=VERTEX_POINT('',#15137);
#4185=VERTEX_POINT('',#15139);
#4186=VERTEX_POINT('',#15143);
#4187=VERTEX_POINT('',#15145);
#4188=VERTEX_POINT('',#15147);
#4189=VERTEX_POINT('',#15149);
#4190=VERTEX_POINT('',#15153);
#4191=VERTEX_POINT('',#15155);
#4192=VERTEX_POINT('',#15157);
#4193=VERTEX_POINT('',#15159);
#4194=VERTEX_POINT('',#15165);
#4195=VERTEX_POINT('',#15169);
#4196=VERTEX_POINT('',#15171);
#4197=VERTEX_POINT('',#15173);
#4198=VERTEX_POINT('',#15175);
#4199=VERTEX_POINT('',#15177);
#4200=VERTEX_POINT('',#15179);
#4201=VERTEX_POINT('',#15181);
#4202=VERTEX_POINT('',#15183);
#4203=VERTEX_POINT('',#15185);
#4204=VERTEX_POINT('',#15187);
#4205=VERTEX_POINT('',#15189);
#4206=VERTEX_POINT('',#15191);
#4207=VERTEX_POINT('',#15193);
#4208=VERTEX_POINT('',#15196);
#4209=VERTEX_POINT('',#15200);
#4210=VERTEX_POINT('',#15204);
#4211=VERTEX_POINT('',#15208);
#4212=VERTEX_POINT('',#15210);
#4213=VERTEX_POINT('',#15214);
#4214=VERTEX_POINT('',#15216);
#4215=VERTEX_POINT('',#15220);
#4216=VERTEX_POINT('',#15222);
#4217=VERTEX_POINT('',#15226);
#4218=VERTEX_POINT('',#15228);
#4219=VERTEX_POINT('',#15234);
#4220=VERTEX_POINT('',#15236);
#4221=VERTEX_POINT('',#15245);
#4222=VERTEX_POINT('',#15247);
#4223=VERTEX_POINT('',#15256);
#4224=VERTEX_POINT('',#15258);
#4225=VERTEX_POINT('',#15262);
#4226=VERTEX_POINT('',#15266);
#4227=VERTEX_POINT('',#15268);
#4228=VERTEX_POINT('',#15277);
#4229=VERTEX_POINT('',#15281);
#4230=VERTEX_POINT('',#15283);
#4231=VERTEX_POINT('',#15287);
#4232=VERTEX_POINT('',#15289);
#4233=VERTEX_POINT('',#15298);
#4234=VERTEX_POINT('',#15300);
#4235=VERTEX_POINT('',#15304);
#4236=VERTEX_POINT('',#15306);
#4237=VERTEX_POINT('',#15312);
#4238=VERTEX_POINT('',#15314);
#4239=VERTEX_POINT('',#15323);
#4240=VERTEX_POINT('',#15332);
#4241=VERTEX_POINT('',#15334);
#4242=VERTEX_POINT('',#15338);
#4243=VERTEX_POINT('',#15344);
#4244=VERTEX_POINT('',#15346);
#4245=VERTEX_POINT('',#15350);
#4246=VERTEX_POINT('',#15356);
#4247=VERTEX_POINT('',#15357);
#4248=VERTEX_POINT('',#15366);
#4249=VERTEX_POINT('',#15368);
#5079=EDGE_CURVE('',#4132,#4132,#3484,.T.);
#5080=EDGE_CURVE('',#4132,#4133,#819,.T.);
#5081=EDGE_CURVE('',#4133,#4133,#3485,.T.);
#5082=EDGE_CURVE('',#4134,#4134,#3486,.T.);
#5083=EDGE_CURVE('',#4134,#4135,#820,.T.);
#5084=EDGE_CURVE('',#4135,#4135,#3487,.T.);
#5085=EDGE_CURVE('',#4136,#4136,#3488,.T.);
#5086=EDGE_CURVE('',#4136,#4137,#821,.T.);
#5087=EDGE_CURVE('',#4137,#4137,#3489,.T.);
#5088=EDGE_CURVE('',#4138,#4138,#3490,.T.);
#5089=EDGE_CURVE('',#4138,#4139,#822,.T.);
#5090=EDGE_CURVE('',#4139,#4139,#3491,.T.);
#5091=EDGE_CURVE('',#4140,#4140,#3492,.T.);
#5092=EDGE_CURVE('',#4140,#4141,#823,.T.);
#5093=EDGE_CURVE('',#4141,#4141,#3493,.T.);
#5094=EDGE_CURVE('',#4142,#4142,#3494,.T.);
#5095=EDGE_CURVE('',#4142,#4143,#824,.T.);
#5096=EDGE_CURVE('',#4143,#4143,#3495,.T.);
#5097=EDGE_CURVE('',#4144,#4144,#3496,.T.);
#5098=EDGE_CURVE('',#4144,#4145,#825,.T.);
#5099=EDGE_CURVE('',#4145,#4145,#3497,.T.);
#5100=EDGE_CURVE('',#4146,#4146,#3498,.T.);
#5101=EDGE_CURVE('',#4146,#4147,#826,.T.);
#5102=EDGE_CURVE('',#4147,#4147,#3499,.T.);
#5103=EDGE_CURVE('',#4148,#4149,#3500,.T.);
#5104=EDGE_CURVE('',#4150,#4148,#827,.T.);
#5105=EDGE_CURVE('',#4150,#4151,#828,.T.);
#5106=EDGE_CURVE('',#4152,#4151,#829,.T.);
#5107=EDGE_CURVE('',#4153,#4152,#3501,.T.);
#5108=EDGE_CURVE('',#4149,#4153,#830,.T.);
#5109=EDGE_CURVE('',#4154,#4155,#3502,.T.);
#5110=EDGE_CURVE('',#4156,#4154,#831,.T.);
#5111=EDGE_CURVE('',#4157,#4156,#3503,.T.);
#5112=EDGE_CURVE('',#4158,#4157,#832,.T.);
#5113=EDGE_CURVE('',#4159,#4158,#833,.T.);
#5114=EDGE_CURVE('',#4155,#4159,#834,.T.);
#5115=EDGE_CURVE('',#4151,#4158,#835,.T.);
#5116=EDGE_CURVE('',#4159,#4150,#836,.T.);
#5117=EDGE_CURVE('',#4155,#4160,#837,.T.);
#5118=EDGE_CURVE('',#4160,#4161,#269,.T.);
#5119=EDGE_CURVE('',#4161,#4154,#838,.T.);
#5120=EDGE_CURVE('',#4149,#4162,#839,.T.);
#5121=EDGE_CURVE('',#4162,#4163,#3504,.F.);
#5122=EDGE_CURVE('',#4163,#4148,#840,.T.);
#5123=EDGE_CURVE('',#4161,#4164,#841,.T.);
#5124=EDGE_CURVE('',#4156,#4164,#842,.T.);
#5125=EDGE_CURVE('',#4165,#4153,#843,.T.);
#5126=EDGE_CURVE('',#4162,#4165,#844,.T.);
#5127=EDGE_CURVE('',#4166,#4164,#270,.T.);
#5128=EDGE_CURVE('',#4166,#4157,#845,.T.);
#5129=EDGE_CURVE('',#4152,#4167,#846,.T.);
#5130=EDGE_CURVE('',#4167,#4165,#3505,.F.);
#5131=EDGE_CURVE('',#4168,#4166,#847,.T.);
#5132=EDGE_CURVE('',#4169,#4168,#848,.T.);
#5133=EDGE_CURVE('',#4169,#4170,#849,.T.);
#5134=EDGE_CURVE('',#4170,#4171,#850,.T.);
#5135=EDGE_CURVE('',#4171,#4172,#851,.T.);
#5136=EDGE_CURVE('',#4173,#4172,#852,.T.);
#5137=EDGE_CURVE('',#4174,#4173,#853,.T.);
#5138=EDGE_CURVE('',#4175,#4174,#854,.T.);
#5139=EDGE_CURVE('',#4176,#4175,#3506,.T.);
#5140=EDGE_CURVE('',#4177,#4176,#855,.T.);
#5141=EDGE_CURVE('',#4178,#4177,#856,.T.);
#5142=EDGE_CURVE('',#4179,#4178,#3507,.T.);
#5143=EDGE_CURVE('',#4180,#4179,#857,.T.);
#5144=EDGE_CURVE('',#4181,#4180,#3508,.T.);
#5145=EDGE_CURVE('',#4182,#4181,#858,.T.);
#5146=EDGE_CURVE('',#4183,#4182,#859,.T.);
#5147=EDGE_CURVE('',#4184,#4183,#3509,.T.);
#5148=EDGE_CURVE('',#4185,#4184,#860,.T.);
#5149=EDGE_CURVE('',#4167,#4185,#861,.T.);
#5150=EDGE_CURVE('',#4172,#4186,#3510,.T.);
#5151=EDGE_CURVE('',#4187,#4171,#862,.T.);
#5152=EDGE_CURVE('',#4188,#4187,#863,.T.);
#5153=EDGE_CURVE('',#4189,#4188,#3511,.T.);
#5154=EDGE_CURVE('',#4186,#4189,#864,.T.);
#5155=EDGE_CURVE('',#4190,#4169,#3512,.T.);
#5156=EDGE_CURVE('',#4191,#4190,#865,.T.);
#5157=EDGE_CURVE('',#4192,#4191,#3513,.T.);
#5158=EDGE_CURVE('',#4193,#4192,#866,.T.);
#5159=EDGE_CURVE('',#4193,#4170,#867,.T.);
#5160=EDGE_CURVE('',#4187,#4193,#868,.T.);
#5161=EDGE_CURVE('',#4186,#4194,#869,.T.);
#5162=EDGE_CURVE('',#4194,#4173,#3514,.F.);
#5163=EDGE_CURVE('',#4195,#4163,#870,.T.);
#5164=EDGE_CURVE('',#4196,#4195,#871,.T.);
#5165=EDGE_CURVE('',#4197,#4196,#3515,.T.);
#5166=EDGE_CURVE('',#4198,#4197,#872,.T.);
#5167=EDGE_CURVE('',#4199,#4198,#873,.T.);
#5168=EDGE_CURVE('',#4200,#4199,#3516,.T.);
#5169=EDGE_CURVE('',#4201,#4200,#874,.T.);
#5170=EDGE_CURVE('',#4202,#4201,#3517,.T.);
#5171=EDGE_CURVE('',#4203,#4202,#875,.T.);
#5172=EDGE_CURVE('',#4204,#4203,#876,.T.);
#5173=EDGE_CURVE('',#4205,#4204,#3518,.T.);
#5174=EDGE_CURVE('',#4206,#4205,#877,.T.);
#5175=EDGE_CURVE('',#4207,#4206,#878,.T.);
#5176=EDGE_CURVE('',#4188,#4207,#879,.T.);
#5177=EDGE_CURVE('',#4208,#4192,#880,.T.);
#5178=EDGE_CURVE('',#4160,#4208,#881,.T.);
#5179=EDGE_CURVE('',#4209,#4189,#882,.T.);
#5180=EDGE_CURVE('',#4194,#4209,#883,.T.);
#5181=EDGE_CURVE('',#4191,#4210,#884,.T.);
#5182=EDGE_CURVE('',#4210,#4208,#3519,.F.);
#5183=EDGE_CURVE('',#4211,#4183,#3520,.T.);
#5184=EDGE_CURVE('',#4212,#4211,#3521,.F.);
#5185=EDGE_CURVE('',#4184,#4212,#3522,.T.);
#5186=EDGE_CURVE('',#4213,#4196,#3523,.T.);
#5187=EDGE_CURVE('',#4214,#4213,#3524,.F.);
#5188=EDGE_CURVE('',#4197,#4214,#3525,.T.);
#5189=EDGE_CURVE('',#4182,#4215,#3526,.F.);
#5190=EDGE_CURVE('',#4216,#4182,#3527,.F.);
#5191=EDGE_CURVE('',#4215,#4216,#3528,.F.);
#5192=EDGE_CURVE('',#4185,#4217,#3529,.F.);
#5193=EDGE_CURVE('',#4218,#4185,#3530,.F.);
#5194=EDGE_CURVE('',#4217,#4218,#3531,.F.);
#5195=EDGE_CURVE('',#4212,#4218,#885,.T.);
#5196=EDGE_CURVE('',#4198,#4219,#3532,.F.);
#5197=EDGE_CURVE('',#4220,#4198,#3533,.F.);
#5198=EDGE_CURVE('',#4219,#4220,#3534,.F.);
#5199=EDGE_CURVE('',#4214,#4220,#886,.T.);
#5200=EDGE_CURVE('',#4220,#4215,#887,.T.);
#5201=EDGE_CURVE('',#4216,#4219,#888,.T.);
#5202=EDGE_CURVE('',#4221,#4195,#3535,.F.);
#5203=EDGE_CURVE('',#4222,#4221,#3536,.F.);
#5204=EDGE_CURVE('',#4195,#4222,#3537,.F.);
#5205=EDGE_CURVE('',#4221,#4217,#889,.T.);
#5206=EDGE_CURVE('',#4218,#4222,#890,.T.);
#5207=EDGE_CURVE('',#4222,#4213,#891,.T.);
#5208=EDGE_CURVE('',#4223,#4180,#3538,.T.);
#5209=EDGE_CURVE('',#4224,#4223,#3539,.F.);
#5210=EDGE_CURVE('',#4181,#4224,#3540,.T.);
#5211=EDGE_CURVE('',#4165,#4225,#3541,.F.);
#5212=EDGE_CURVE('',#4225,#4167,#3542,.F.);
#5213=EDGE_CURVE('',#4226,#4199,#3543,.T.);
#5214=EDGE_CURVE('',#4227,#4226,#3544,.F.);
#5215=EDGE_CURVE('',#4200,#4227,#3545,.T.);
#5216=EDGE_CURVE('',#4219,#4226,#892,.T.);
#5217=EDGE_CURVE('',#4226,#4224,#893,.T.);
#5218=EDGE_CURVE('',#4223,#4227,#894,.T.);
#5219=EDGE_CURVE('',#4163,#4228,#3546,.F.);
#5220=EDGE_CURVE('',#4228,#4162,#3547,.F.);
#5221=EDGE_CURVE('',#4229,#4178,#3548,.T.);
#5222=EDGE_CURVE('',#4230,#4229,#3549,.F.);
#5223=EDGE_CURVE('',#4179,#4230,#3550,.T.);
#5224=EDGE_CURVE('',#4231,#4201,#3551,.T.);
#5225=EDGE_CURVE('',#4232,#4231,#3552,.F.);
#5226=EDGE_CURVE('',#4202,#4232,#3553,.T.);
#5227=EDGE_CURVE('',#4227,#4231,#895,.T.);
#5228=EDGE_CURVE('',#4231,#4230,#896,.T.);
#5229=EDGE_CURVE('',#4229,#4232,#897,.T.);
#5230=EDGE_CURVE('',#4177,#4233,#3554,.F.);
#5231=EDGE_CURVE('',#4234,#4177,#3555,.F.);
#5232=EDGE_CURVE('',#4233,#4234,#3556,.F.);
#5233=EDGE_CURVE('',#4168,#4235,#3557,.F.);
#5234=EDGE_CURVE('',#4236,#4168,#3558,.F.);
#5235=EDGE_CURVE('',#4235,#4236,#3559,.F.);
#5236=EDGE_CURVE('',#4164,#4236,#898,.T.);
#5237=EDGE_CURVE('',#4203,#4237,#3560,.F.);
#5238=EDGE_CURVE('',#4238,#4203,#3561,.F.);
#5239=EDGE_CURVE('',#4237,#4238,#3562,.F.);
#5240=EDGE_CURVE('',#4232,#4238,#899,.T.);
#5241=EDGE_CURVE('',#4238,#4233,#900,.T.);
#5242=EDGE_CURVE('',#4234,#4237,#901,.T.);
#5243=EDGE_CURVE('',#4239,#4210,#3563,.F.);
#5244=EDGE_CURVE('',#4208,#4239,#3564,.F.);
#5245=EDGE_CURVE('',#4210,#4235,#902,.T.);
#5246=EDGE_CURVE('',#4236,#4239,#903,.T.);
#5247=EDGE_CURVE('',#4239,#4161,#904,.T.);
#5248=EDGE_CURVE('',#4240,#4175,#3565,.T.);
#5249=EDGE_CURVE('',#4241,#4240,#3566,.F.);
#5250=EDGE_CURVE('',#4176,#4241,#3567,.T.);
#5251=EDGE_CURVE('',#4173,#4242,#3568,.F.);
#5252=EDGE_CURVE('',#4242,#4194,#3569,.F.);
#5253=EDGE_CURVE('',#4235,#4190,#905,.T.);
#5254=EDGE_CURVE('',#4243,#4204,#3570,.T.);
#5255=EDGE_CURVE('',#4244,#4243,#3571,.F.);
#5256=EDGE_CURVE('',#4205,#4244,#3572,.T.);
#5257=EDGE_CURVE('',#4209,#4245,#3573,.F.);
#5258=EDGE_CURVE('',#4207,#4209,#3574,.F.);
#5259=EDGE_CURVE('',#4245,#4207,#3575,.F.);
#5260=EDGE_CURVE('',#4246,#4247,#3576,.F.);
#5261=EDGE_CURVE('',#4174,#4246,#3577,.F.);
#5262=EDGE_CURVE('',#4247,#4174,#3578,.F.);
#5263=EDGE_CURVE('',#4246,#4240,#906,.T.);
#5264=EDGE_CURVE('',#4242,#4247,#907,.T.);
#5265=EDGE_CURVE('',#4248,#4206,#3579,.F.);
#5266=EDGE_CURVE('',#4249,#4248,#3580,.F.);
#5267=EDGE_CURVE('',#4206,#4249,#3581,.F.);
#5268=EDGE_CURVE('',#4247,#4249,#908,.T.);
#5269=EDGE_CURVE('',#4248,#4246,#909,.T.);
#5270=EDGE_CURVE('',#4249,#4245,#910,.T.);
#5271=EDGE_CURVE('',#4244,#4248,#911,.T.);
#5272=EDGE_CURVE('',#4245,#4242,#912,.T.);
#5273=EDGE_CURVE('',#4237,#4243,#913,.T.);
#5274=EDGE_CURVE('',#4243,#4241,#914,.T.);
#5275=EDGE_CURVE('',#4240,#4244,#915,.T.);
#5276=EDGE_CURVE('',#4241,#4234,#916,.T.);
#5277=EDGE_CURVE('',#4233,#4229,#917,.T.);
#5278=EDGE_CURVE('',#4230,#4223,#918,.T.);
#5279=EDGE_CURVE('',#4225,#4228,#919,.T.);
#5280=EDGE_CURVE('',#4228,#4221,#920,.T.);
#5281=EDGE_CURVE('',#4217,#4225,#921,.T.);
#5282=EDGE_CURVE('',#4224,#4216,#922,.T.);
#5283=EDGE_CURVE('',#4215,#4211,#923,.T.);
#5284=EDGE_CURVE('',#4213,#4212,#924,.T.);
#5285=EDGE_CURVE('',#4211,#4214,#925,.T.);
#6817=ORIENTED_EDGE('',*,*,#5079,.F.);
#6818=ORIENTED_EDGE('',*,*,#5080,.T.);
#6819=ORIENTED_EDGE('',*,*,#5081,.F.);
#6820=ORIENTED_EDGE('',*,*,#5080,.F.);
#6821=ORIENTED_EDGE('',*,*,#5081,.T.);
#6822=ORIENTED_EDGE('',*,*,#5082,.F.);
#6823=ORIENTED_EDGE('',*,*,#5083,.T.);
#6824=ORIENTED_EDGE('',*,*,#5084,.F.);
#6825=ORIENTED_EDGE('',*,*,#5083,.F.);
#6826=ORIENTED_EDGE('',*,*,#5084,.T.);
#6827=ORIENTED_EDGE('',*,*,#5085,.F.);
#6828=ORIENTED_EDGE('',*,*,#5086,.T.);
#6829=ORIENTED_EDGE('',*,*,#5087,.F.);
#6830=ORIENTED_EDGE('',*,*,#5086,.F.);
#6831=ORIENTED_EDGE('',*,*,#5087,.T.);
#6832=ORIENTED_EDGE('',*,*,#5088,.F.);
#6833=ORIENTED_EDGE('',*,*,#5089,.T.);
#6834=ORIENTED_EDGE('',*,*,#5090,.F.);
#6835=ORIENTED_EDGE('',*,*,#5089,.F.);
#6836=ORIENTED_EDGE('',*,*,#5090,.T.);
#6837=ORIENTED_EDGE('',*,*,#5091,.F.);
#6838=ORIENTED_EDGE('',*,*,#5092,.T.);
#6839=ORIENTED_EDGE('',*,*,#5093,.T.);
#6840=ORIENTED_EDGE('',*,*,#5092,.F.);
#6841=ORIENTED_EDGE('',*,*,#5093,.F.);
#6842=ORIENTED_EDGE('',*,*,#5094,.F.);
#6843=ORIENTED_EDGE('',*,*,#5095,.T.);
#6844=ORIENTED_EDGE('',*,*,#5096,.T.);
#6845=ORIENTED_EDGE('',*,*,#5095,.F.);
#6846=ORIENTED_EDGE('',*,*,#5096,.F.);
#6847=ORIENTED_EDGE('',*,*,#5097,.F.);
#6848=ORIENTED_EDGE('',*,*,#5098,.T.);
#6849=ORIENTED_EDGE('',*,*,#5099,.T.);
#6850=ORIENTED_EDGE('',*,*,#5098,.F.);
#6851=ORIENTED_EDGE('',*,*,#5099,.F.);
#6852=ORIENTED_EDGE('',*,*,#5100,.F.);
#6853=ORIENTED_EDGE('',*,*,#5101,.T.);
#6854=ORIENTED_EDGE('',*,*,#5102,.T.);
#6855=ORIENTED_EDGE('',*,*,#5101,.F.);
#6856=ORIENTED_EDGE('',*,*,#5102,.F.);
#6857=ORIENTED_EDGE('',*,*,#5103,.F.);
#6858=ORIENTED_EDGE('',*,*,#5104,.F.);
#6859=ORIENTED_EDGE('',*,*,#5105,.T.);
#6860=ORIENTED_EDGE('',*,*,#5106,.F.);
#6861=ORIENTED_EDGE('',*,*,#5107,.F.);
#6862=ORIENTED_EDGE('',*,*,#5108,.F.);
#6863=ORIENTED_EDGE('',*,*,#5109,.F.);
#6864=ORIENTED_EDGE('',*,*,#5110,.F.);
#6865=ORIENTED_EDGE('',*,*,#5111,.F.);
#6866=ORIENTED_EDGE('',*,*,#5112,.F.);
#6867=ORIENTED_EDGE('',*,*,#5113,.F.);
#6868=ORIENTED_EDGE('',*,*,#5114,.F.);
#6869=ORIENTED_EDGE('',*,*,#5113,.T.);
#6870=ORIENTED_EDGE('',*,*,#5115,.F.);
#6871=ORIENTED_EDGE('',*,*,#5105,.F.);
#6872=ORIENTED_EDGE('',*,*,#5116,.F.);
#6873=ORIENTED_EDGE('',*,*,#5109,.T.);
#6874=ORIENTED_EDGE('',*,*,#5117,.T.);
#6875=ORIENTED_EDGE('',*,*,#5118,.T.);
#6876=ORIENTED_EDGE('',*,*,#5119,.T.);
#6877=ORIENTED_EDGE('',*,*,#5103,.T.);
#6878=ORIENTED_EDGE('',*,*,#5120,.T.);
#6879=ORIENTED_EDGE('',*,*,#5121,.T.);
#6880=ORIENTED_EDGE('',*,*,#5122,.T.);
#6881=ORIENTED_EDGE('',*,*,#5110,.T.);
#6882=ORIENTED_EDGE('',*,*,#5119,.F.);
#6883=ORIENTED_EDGE('',*,*,#5123,.T.);
#6884=ORIENTED_EDGE('',*,*,#5124,.F.);
#6885=ORIENTED_EDGE('',*,*,#5108,.T.);
#6886=ORIENTED_EDGE('',*,*,#5125,.F.);
#6887=ORIENTED_EDGE('',*,*,#5126,.F.);
#6888=ORIENTED_EDGE('',*,*,#5120,.F.);
#6889=ORIENTED_EDGE('',*,*,#5091,.T.);
#6890=ORIENTED_EDGE('',*,*,#5094,.T.);
#6891=ORIENTED_EDGE('',*,*,#5097,.T.);
#6892=ORIENTED_EDGE('',*,*,#5100,.T.);
#6893=ORIENTED_EDGE('',*,*,#5111,.T.);
#6894=ORIENTED_EDGE('',*,*,#5124,.T.);
#6895=ORIENTED_EDGE('',*,*,#5127,.F.);
#6896=ORIENTED_EDGE('',*,*,#5128,.T.);
#6897=ORIENTED_EDGE('',*,*,#5107,.T.);
#6898=ORIENTED_EDGE('',*,*,#5129,.T.);
#6899=ORIENTED_EDGE('',*,*,#5130,.T.);
#6900=ORIENTED_EDGE('',*,*,#5125,.T.);
#6901=ORIENTED_EDGE('',*,*,#5106,.T.);
#6902=ORIENTED_EDGE('',*,*,#5115,.T.);
#6903=ORIENTED_EDGE('',*,*,#5112,.T.);
#6904=ORIENTED_EDGE('',*,*,#5128,.F.);
#6905=ORIENTED_EDGE('',*,*,#5131,.F.);
#6906=ORIENTED_EDGE('',*,*,#5132,.F.);
#6907=ORIENTED_EDGE('',*,*,#5133,.T.);
#6908=ORIENTED_EDGE('',*,*,#5134,.T.);
#6909=ORIENTED_EDGE('',*,*,#5135,.T.);
#6910=ORIENTED_EDGE('',*,*,#5136,.F.);
#6911=ORIENTED_EDGE('',*,*,#5137,.F.);
#6912=ORIENTED_EDGE('',*,*,#5138,.F.);
#6913=ORIENTED_EDGE('',*,*,#5139,.F.);
#6914=ORIENTED_EDGE('',*,*,#5140,.F.);
#6915=ORIENTED_EDGE('',*,*,#5141,.F.);
#6916=ORIENTED_EDGE('',*,*,#5142,.F.);
#6917=ORIENTED_EDGE('',*,*,#5143,.F.);
#6918=ORIENTED_EDGE('',*,*,#5144,.F.);
#6919=ORIENTED_EDGE('',*,*,#5145,.F.);
#6920=ORIENTED_EDGE('',*,*,#5146,.F.);
#6921=ORIENTED_EDGE('',*,*,#5147,.F.);
#6922=ORIENTED_EDGE('',*,*,#5148,.F.);
#6923=ORIENTED_EDGE('',*,*,#5149,.F.);
#6924=ORIENTED_EDGE('',*,*,#5129,.F.);
#6925=ORIENTED_EDGE('',*,*,#5150,.F.);
#6926=ORIENTED_EDGE('',*,*,#5135,.F.);
#6927=ORIENTED_EDGE('',*,*,#5151,.F.);
#6928=ORIENTED_EDGE('',*,*,#5152,.F.);
#6929=ORIENTED_EDGE('',*,*,#5153,.F.);
#6930=ORIENTED_EDGE('',*,*,#5154,.F.);
#6931=ORIENTED_EDGE('',*,*,#5155,.F.);
#6932=ORIENTED_EDGE('',*,*,#5156,.F.);
#6933=ORIENTED_EDGE('',*,*,#5157,.F.);
#6934=ORIENTED_EDGE('',*,*,#5158,.F.);
#6935=ORIENTED_EDGE('',*,*,#5159,.T.);
#6936=ORIENTED_EDGE('',*,*,#5133,.F.);
#6937=ORIENTED_EDGE('',*,*,#5159,.F.);
#6938=ORIENTED_EDGE('',*,*,#5160,.F.);
#6939=ORIENTED_EDGE('',*,*,#5151,.T.);
#6940=ORIENTED_EDGE('',*,*,#5134,.F.);
#6941=ORIENTED_EDGE('',*,*,#5150,.T.);
#6942=ORIENTED_EDGE('',*,*,#5161,.T.);
#6943=ORIENTED_EDGE('',*,*,#5162,.T.);
#6944=ORIENTED_EDGE('',*,*,#5136,.T.);
#6945=ORIENTED_EDGE('',*,*,#5104,.T.);
#6946=ORIENTED_EDGE('',*,*,#5122,.F.);
#6947=ORIENTED_EDGE('',*,*,#5163,.F.);
#6948=ORIENTED_EDGE('',*,*,#5164,.F.);
#6949=ORIENTED_EDGE('',*,*,#5165,.F.);
#6950=ORIENTED_EDGE('',*,*,#5166,.F.);
#6951=ORIENTED_EDGE('',*,*,#5167,.F.);
#6952=ORIENTED_EDGE('',*,*,#5168,.F.);
#6953=ORIENTED_EDGE('',*,*,#5169,.F.);
#6954=ORIENTED_EDGE('',*,*,#5170,.F.);
#6955=ORIENTED_EDGE('',*,*,#5171,.F.);
#6956=ORIENTED_EDGE('',*,*,#5172,.F.);
#6957=ORIENTED_EDGE('',*,*,#5173,.F.);
#6958=ORIENTED_EDGE('',*,*,#5174,.F.);
#6959=ORIENTED_EDGE('',*,*,#5175,.F.);
#6960=ORIENTED_EDGE('',*,*,#5176,.F.);
#6961=ORIENTED_EDGE('',*,*,#5152,.T.);
#6962=ORIENTED_EDGE('',*,*,#5160,.T.);
#6963=ORIENTED_EDGE('',*,*,#5158,.T.);
#6964=ORIENTED_EDGE('',*,*,#5177,.F.);
#6965=ORIENTED_EDGE('',*,*,#5178,.F.);
#6966=ORIENTED_EDGE('',*,*,#5117,.F.);
#6967=ORIENTED_EDGE('',*,*,#5114,.T.);
#6968=ORIENTED_EDGE('',*,*,#5116,.T.);
#6969=ORIENTED_EDGE('',*,*,#5154,.T.);
#6970=ORIENTED_EDGE('',*,*,#5179,.F.);
#6971=ORIENTED_EDGE('',*,*,#5180,.F.);
#6972=ORIENTED_EDGE('',*,*,#5161,.F.);
#6973=ORIENTED_EDGE('',*,*,#5079,.T.);
#6974=ORIENTED_EDGE('',*,*,#5082,.T.);
#6975=ORIENTED_EDGE('',*,*,#5085,.T.);
#6976=ORIENTED_EDGE('',*,*,#5088,.T.);
#6977=ORIENTED_EDGE('',*,*,#5157,.T.);
#6978=ORIENTED_EDGE('',*,*,#5181,.T.);
#6979=ORIENTED_EDGE('',*,*,#5182,.T.);
#6980=ORIENTED_EDGE('',*,*,#5177,.T.);
#6981=ORIENTED_EDGE('',*,*,#5147,.T.);
#6982=ORIENTED_EDGE('',*,*,#5183,.F.);
#6983=ORIENTED_EDGE('',*,*,#5184,.F.);
#6984=ORIENTED_EDGE('',*,*,#5185,.F.);
#6985=ORIENTED_EDGE('',*,*,#5165,.T.);
#6986=ORIENTED_EDGE('',*,*,#5186,.F.);
#6987=ORIENTED_EDGE('',*,*,#5187,.F.);
#6988=ORIENTED_EDGE('',*,*,#5188,.F.);
#6989=ORIENTED_EDGE('',*,*,#5189,.F.);
#6990=ORIENTED_EDGE('',*,*,#5190,.F.);
#6991=ORIENTED_EDGE('',*,*,#5191,.F.);
#6992=ORIENTED_EDGE('',*,*,#5192,.F.);
#6993=ORIENTED_EDGE('',*,*,#5193,.F.);
#6994=ORIENTED_EDGE('',*,*,#5194,.F.);
#6995=ORIENTED_EDGE('',*,*,#5193,.T.);
#6996=ORIENTED_EDGE('',*,*,#5148,.T.);
#6997=ORIENTED_EDGE('',*,*,#5185,.T.);
#6998=ORIENTED_EDGE('',*,*,#5195,.T.);
#6999=ORIENTED_EDGE('',*,*,#5196,.F.);
#7000=ORIENTED_EDGE('',*,*,#5197,.F.);
#7001=ORIENTED_EDGE('',*,*,#5198,.F.);
#7002=ORIENTED_EDGE('',*,*,#5197,.T.);
#7003=ORIENTED_EDGE('',*,*,#5166,.T.);
#7004=ORIENTED_EDGE('',*,*,#5188,.T.);
#7005=ORIENTED_EDGE('',*,*,#5199,.T.);
#7006=ORIENTED_EDGE('',*,*,#5198,.T.);
#7007=ORIENTED_EDGE('',*,*,#5200,.T.);
#7008=ORIENTED_EDGE('',*,*,#5191,.T.);
#7009=ORIENTED_EDGE('',*,*,#5201,.T.);
#7010=ORIENTED_EDGE('',*,*,#5202,.F.);
#7011=ORIENTED_EDGE('',*,*,#5203,.F.);
#7012=ORIENTED_EDGE('',*,*,#5204,.F.);
#7013=ORIENTED_EDGE('',*,*,#5203,.T.);
#7014=ORIENTED_EDGE('',*,*,#5205,.T.);
#7015=ORIENTED_EDGE('',*,*,#5194,.T.);
#7016=ORIENTED_EDGE('',*,*,#5206,.T.);
#7017=ORIENTED_EDGE('',*,*,#5186,.T.);
#7018=ORIENTED_EDGE('',*,*,#5164,.T.);
#7019=ORIENTED_EDGE('',*,*,#5204,.T.);
#7020=ORIENTED_EDGE('',*,*,#5207,.T.);
#7021=ORIENTED_EDGE('',*,*,#5144,.T.);
#7022=ORIENTED_EDGE('',*,*,#5208,.F.);
#7023=ORIENTED_EDGE('',*,*,#5209,.F.);
#7024=ORIENTED_EDGE('',*,*,#5210,.F.);
#7025=ORIENTED_EDGE('',*,*,#5211,.F.);
#7026=ORIENTED_EDGE('',*,*,#5130,.F.);
#7027=ORIENTED_EDGE('',*,*,#5212,.F.);
#7028=ORIENTED_EDGE('',*,*,#5168,.T.);
#7029=ORIENTED_EDGE('',*,*,#5213,.F.);
#7030=ORIENTED_EDGE('',*,*,#5214,.F.);
#7031=ORIENTED_EDGE('',*,*,#5215,.F.);
#7032=ORIENTED_EDGE('',*,*,#5213,.T.);
#7033=ORIENTED_EDGE('',*,*,#5167,.T.);
#7034=ORIENTED_EDGE('',*,*,#5196,.T.);
#7035=ORIENTED_EDGE('',*,*,#5216,.T.);
#7036=ORIENTED_EDGE('',*,*,#5214,.T.);
#7037=ORIENTED_EDGE('',*,*,#5217,.T.);
#7038=ORIENTED_EDGE('',*,*,#5209,.T.);
#7039=ORIENTED_EDGE('',*,*,#5218,.T.);
#7040=ORIENTED_EDGE('',*,*,#5219,.F.);
#7041=ORIENTED_EDGE('',*,*,#5121,.F.);
#7042=ORIENTED_EDGE('',*,*,#5220,.F.);
#7043=ORIENTED_EDGE('',*,*,#5142,.T.);
#7044=ORIENTED_EDGE('',*,*,#5221,.F.);
#7045=ORIENTED_EDGE('',*,*,#5222,.F.);
#7046=ORIENTED_EDGE('',*,*,#5223,.F.);
#7047=ORIENTED_EDGE('',*,*,#5170,.T.);
#7048=ORIENTED_EDGE('',*,*,#5224,.F.);
#7049=ORIENTED_EDGE('',*,*,#5225,.F.);
#7050=ORIENTED_EDGE('',*,*,#5226,.F.);
#7051=ORIENTED_EDGE('',*,*,#5224,.T.);
#7052=ORIENTED_EDGE('',*,*,#5169,.T.);
#7053=ORIENTED_EDGE('',*,*,#5215,.T.);
#7054=ORIENTED_EDGE('',*,*,#5227,.T.);
#7055=ORIENTED_EDGE('',*,*,#5225,.T.);
#7056=ORIENTED_EDGE('',*,*,#5228,.T.);
#7057=ORIENTED_EDGE('',*,*,#5222,.T.);
#7058=ORIENTED_EDGE('',*,*,#5229,.T.);
#7059=ORIENTED_EDGE('',*,*,#5230,.F.);
#7060=ORIENTED_EDGE('',*,*,#5231,.F.);
#7061=ORIENTED_EDGE('',*,*,#5232,.F.);
#7062=ORIENTED_EDGE('',*,*,#5233,.F.);
#7063=ORIENTED_EDGE('',*,*,#5234,.F.);
#7064=ORIENTED_EDGE('',*,*,#5235,.F.);
#7065=ORIENTED_EDGE('',*,*,#5236,.T.);
#7066=ORIENTED_EDGE('',*,*,#5234,.T.);
#7067=ORIENTED_EDGE('',*,*,#5131,.T.);
#7068=ORIENTED_EDGE('',*,*,#5127,.T.);
#7069=ORIENTED_EDGE('',*,*,#5237,.F.);
#7070=ORIENTED_EDGE('',*,*,#5238,.F.);
#7071=ORIENTED_EDGE('',*,*,#5239,.F.);
#7072=ORIENTED_EDGE('',*,*,#5238,.T.);
#7073=ORIENTED_EDGE('',*,*,#5171,.T.);
#7074=ORIENTED_EDGE('',*,*,#5226,.T.);
#7075=ORIENTED_EDGE('',*,*,#5240,.T.);
#7076=ORIENTED_EDGE('',*,*,#5239,.T.);
#7077=ORIENTED_EDGE('',*,*,#5241,.T.);
#7078=ORIENTED_EDGE('',*,*,#5232,.T.);
#7079=ORIENTED_EDGE('',*,*,#5242,.T.);
#7080=ORIENTED_EDGE('',*,*,#5182,.F.);
#7081=ORIENTED_EDGE('',*,*,#5243,.F.);
#7082=ORIENTED_EDGE('',*,*,#5244,.F.);
#7083=ORIENTED_EDGE('',*,*,#5243,.T.);
#7084=ORIENTED_EDGE('',*,*,#5245,.T.);
#7085=ORIENTED_EDGE('',*,*,#5235,.T.);
#7086=ORIENTED_EDGE('',*,*,#5246,.T.);
#7087=ORIENTED_EDGE('',*,*,#5178,.T.);
#7088=ORIENTED_EDGE('',*,*,#5244,.T.);
#7089=ORIENTED_EDGE('',*,*,#5247,.T.);
#7090=ORIENTED_EDGE('',*,*,#5118,.F.);
#7091=ORIENTED_EDGE('',*,*,#5139,.T.);
#7092=ORIENTED_EDGE('',*,*,#5248,.F.);
#7093=ORIENTED_EDGE('',*,*,#5249,.F.);
#7094=ORIENTED_EDGE('',*,*,#5250,.F.);
#7095=ORIENTED_EDGE('',*,*,#5251,.F.);
#7096=ORIENTED_EDGE('',*,*,#5162,.F.);
#7097=ORIENTED_EDGE('',*,*,#5252,.F.);
#7098=ORIENTED_EDGE('',*,*,#5155,.T.);
#7099=ORIENTED_EDGE('',*,*,#5132,.T.);
#7100=ORIENTED_EDGE('',*,*,#5233,.T.);
#7101=ORIENTED_EDGE('',*,*,#5253,.T.);
#7102=ORIENTED_EDGE('',*,*,#5173,.T.);
#7103=ORIENTED_EDGE('',*,*,#5254,.F.);
#7104=ORIENTED_EDGE('',*,*,#5255,.F.);
#7105=ORIENTED_EDGE('',*,*,#5256,.F.);
#7106=ORIENTED_EDGE('',*,*,#5257,.F.);
#7107=ORIENTED_EDGE('',*,*,#5258,.F.);
#7108=ORIENTED_EDGE('',*,*,#5259,.F.);
#7109=ORIENTED_EDGE('',*,*,#5153,.T.);
#7110=ORIENTED_EDGE('',*,*,#5176,.T.);
#7111=ORIENTED_EDGE('',*,*,#5258,.T.);
#7112=ORIENTED_EDGE('',*,*,#5179,.T.);
#7113=ORIENTED_EDGE('',*,*,#5260,.F.);
#7114=ORIENTED_EDGE('',*,*,#5261,.F.);
#7115=ORIENTED_EDGE('',*,*,#5262,.F.);
#7116=ORIENTED_EDGE('',*,*,#5248,.T.);
#7117=ORIENTED_EDGE('',*,*,#5138,.T.);
#7118=ORIENTED_EDGE('',*,*,#5261,.T.);
#7119=ORIENTED_EDGE('',*,*,#5263,.T.);
#7120=ORIENTED_EDGE('',*,*,#5251,.T.);
#7121=ORIENTED_EDGE('',*,*,#5264,.T.);
#7122=ORIENTED_EDGE('',*,*,#5262,.T.);
#7123=ORIENTED_EDGE('',*,*,#5137,.T.);
#7124=ORIENTED_EDGE('',*,*,#5265,.F.);
#7125=ORIENTED_EDGE('',*,*,#5266,.F.);
#7126=ORIENTED_EDGE('',*,*,#5267,.F.);
#7127=ORIENTED_EDGE('',*,*,#5260,.T.);
#7128=ORIENTED_EDGE('',*,*,#5268,.T.);
#7129=ORIENTED_EDGE('',*,*,#5266,.T.);
#7130=ORIENTED_EDGE('',*,*,#5269,.T.);
#7131=ORIENTED_EDGE('',*,*,#5267,.T.);
#7132=ORIENTED_EDGE('',*,*,#5270,.T.);
#7133=ORIENTED_EDGE('',*,*,#5259,.T.);
#7134=ORIENTED_EDGE('',*,*,#5175,.T.);
#7135=ORIENTED_EDGE('',*,*,#5265,.T.);
#7136=ORIENTED_EDGE('',*,*,#5174,.T.);
#7137=ORIENTED_EDGE('',*,*,#5256,.T.);
#7138=ORIENTED_EDGE('',*,*,#5271,.T.);
#7139=ORIENTED_EDGE('',*,*,#5257,.T.);
#7140=ORIENTED_EDGE('',*,*,#5272,.T.);
#7141=ORIENTED_EDGE('',*,*,#5252,.T.);
#7142=ORIENTED_EDGE('',*,*,#5180,.T.);
#7143=ORIENTED_EDGE('',*,*,#5254,.T.);
#7144=ORIENTED_EDGE('',*,*,#5172,.T.);
#7145=ORIENTED_EDGE('',*,*,#5237,.T.);
#7146=ORIENTED_EDGE('',*,*,#5273,.T.);
#7147=ORIENTED_EDGE('',*,*,#5255,.T.);
#7148=ORIENTED_EDGE('',*,*,#5274,.T.);
#7149=ORIENTED_EDGE('',*,*,#5249,.T.);
#7150=ORIENTED_EDGE('',*,*,#5275,.T.);
#7151=ORIENTED_EDGE('',*,*,#5231,.T.);
#7152=ORIENTED_EDGE('',*,*,#5140,.T.);
#7153=ORIENTED_EDGE('',*,*,#5250,.T.);
#7154=ORIENTED_EDGE('',*,*,#5276,.T.);
#7155=ORIENTED_EDGE('',*,*,#5221,.T.);
#7156=ORIENTED_EDGE('',*,*,#5141,.T.);
#7157=ORIENTED_EDGE('',*,*,#5230,.T.);
#7158=ORIENTED_EDGE('',*,*,#5277,.T.);
#7159=ORIENTED_EDGE('',*,*,#5208,.T.);
#7160=ORIENTED_EDGE('',*,*,#5143,.T.);
#7161=ORIENTED_EDGE('',*,*,#5223,.T.);
#7162=ORIENTED_EDGE('',*,*,#5278,.T.);
#7163=ORIENTED_EDGE('',*,*,#5211,.T.);
#7164=ORIENTED_EDGE('',*,*,#5279,.T.);
#7165=ORIENTED_EDGE('',*,*,#5220,.T.);
#7166=ORIENTED_EDGE('',*,*,#5126,.T.);
#7167=ORIENTED_EDGE('',*,*,#5219,.T.);
#7168=ORIENTED_EDGE('',*,*,#5280,.T.);
#7169=ORIENTED_EDGE('',*,*,#5202,.T.);
#7170=ORIENTED_EDGE('',*,*,#5163,.T.);
#7171=ORIENTED_EDGE('',*,*,#5192,.T.);
#7172=ORIENTED_EDGE('',*,*,#5281,.T.);
#7173=ORIENTED_EDGE('',*,*,#5212,.T.);
#7174=ORIENTED_EDGE('',*,*,#5149,.T.);
#7175=ORIENTED_EDGE('',*,*,#5190,.T.);
#7176=ORIENTED_EDGE('',*,*,#5145,.T.);
#7177=ORIENTED_EDGE('',*,*,#5210,.T.);
#7178=ORIENTED_EDGE('',*,*,#5282,.T.);
#7179=ORIENTED_EDGE('',*,*,#5183,.T.);
#7180=ORIENTED_EDGE('',*,*,#5146,.T.);
#7181=ORIENTED_EDGE('',*,*,#5189,.T.);
#7182=ORIENTED_EDGE('',*,*,#5283,.T.);
#7183=ORIENTED_EDGE('',*,*,#5187,.T.);
#7184=ORIENTED_EDGE('',*,*,#5284,.T.);
#7185=ORIENTED_EDGE('',*,*,#5184,.T.);
#7186=ORIENTED_EDGE('',*,*,#5285,.T.);
#7187=ORIENTED_EDGE('',*,*,#5247,.F.);
#7188=ORIENTED_EDGE('',*,*,#5246,.F.);
#7189=ORIENTED_EDGE('',*,*,#5236,.F.);
#7190=ORIENTED_EDGE('',*,*,#5123,.F.);
#7191=ORIENTED_EDGE('',*,*,#5195,.F.);
#7192=ORIENTED_EDGE('',*,*,#5284,.F.);
#7193=ORIENTED_EDGE('',*,*,#5207,.F.);
#7194=ORIENTED_EDGE('',*,*,#5206,.F.);
#7195=ORIENTED_EDGE('',*,*,#5199,.F.);
#7196=ORIENTED_EDGE('',*,*,#5285,.F.);
#7197=ORIENTED_EDGE('',*,*,#5283,.F.);
#7198=ORIENTED_EDGE('',*,*,#5200,.F.);
#7199=ORIENTED_EDGE('',*,*,#5201,.F.);
#7200=ORIENTED_EDGE('',*,*,#5282,.F.);
#7201=ORIENTED_EDGE('',*,*,#5217,.F.);
#7202=ORIENTED_EDGE('',*,*,#5216,.F.);
#7203=ORIENTED_EDGE('',*,*,#5218,.F.);
#7204=ORIENTED_EDGE('',*,*,#5278,.F.);
#7205=ORIENTED_EDGE('',*,*,#5228,.F.);
#7206=ORIENTED_EDGE('',*,*,#5227,.F.);
#7207=ORIENTED_EDGE('',*,*,#5229,.F.);
#7208=ORIENTED_EDGE('',*,*,#5277,.F.);
#7209=ORIENTED_EDGE('',*,*,#5241,.F.);
#7210=ORIENTED_EDGE('',*,*,#5240,.F.);
#7211=ORIENTED_EDGE('',*,*,#5242,.F.);
#7212=ORIENTED_EDGE('',*,*,#5276,.F.);
#7213=ORIENTED_EDGE('',*,*,#5274,.F.);
#7214=ORIENTED_EDGE('',*,*,#5273,.F.);
#7215=ORIENTED_EDGE('',*,*,#5156,.T.);
#7216=ORIENTED_EDGE('',*,*,#5253,.F.);
#7217=ORIENTED_EDGE('',*,*,#5245,.F.);
#7218=ORIENTED_EDGE('',*,*,#5181,.F.);
#7219=ORIENTED_EDGE('',*,*,#5263,.F.);
#7220=ORIENTED_EDGE('',*,*,#5269,.F.);
#7221=ORIENTED_EDGE('',*,*,#5271,.F.);
#7222=ORIENTED_EDGE('',*,*,#5275,.F.);
#7223=ORIENTED_EDGE('',*,*,#5264,.F.);
#7224=ORIENTED_EDGE('',*,*,#5272,.F.);
#7225=ORIENTED_EDGE('',*,*,#5270,.F.);
#7226=ORIENTED_EDGE('',*,*,#5268,.F.);
#7227=ORIENTED_EDGE('',*,*,#5279,.F.);
#7228=ORIENTED_EDGE('',*,*,#5281,.F.);
#7229=ORIENTED_EDGE('',*,*,#5205,.F.);
#7230=ORIENTED_EDGE('',*,*,#5280,.F.);
#8906=PLANE('',#10105);
#8907=PLANE('',#10109);
#8908=PLANE('',#10113);
#8909=PLANE('',#10117);
#8910=PLANE('',#10121);
#8911=PLANE('',#10125);
#8912=PLANE('',#10129);
#8913=PLANE('',#10133);
#8914=PLANE('',#10134);
#8915=PLANE('',#10137);
#8916=PLANE('',#10140);
#8917=PLANE('',#10145);
#8918=PLANE('',#10146);
#8919=PLANE('',#10151);
#8920=PLANE('',#10156);
#8921=PLANE('',#10159);
#8922=PLANE('',#10162);
#8923=PLANE('',#10165);
#8924=PLANE('',#10170);
#8925=PLANE('',#10290);
#8926=PLANE('',#10291);
#8927=PLANE('',#10292);
#8928=PLANE('',#10293);
#8929=PLANE('',#10294);
#8930=PLANE('',#10295);
#8931=PLANE('',#10296);
#8932=PLANE('',#10297);
#8933=PLANE('',#10298);
#8934=PLANE('',#10299);
#8935=PLANE('',#10300);
#9184=ADVANCED_FACE('',(#2197),#408,.F.);
#9185=ADVANCED_FACE('',(#2198),#8906,.F.);
#9186=ADVANCED_FACE('',(#2199),#409,.F.);
#9187=ADVANCED_FACE('',(#2200),#8907,.F.);
#9188=ADVANCED_FACE('',(#2201),#410,.F.);
#9189=ADVANCED_FACE('',(#2202),#8908,.F.);
#9190=ADVANCED_FACE('',(#2203),#411,.F.);
#9191=ADVANCED_FACE('',(#2204),#8909,.F.);
#9192=ADVANCED_FACE('',(#2205),#412,.F.);
#9193=ADVANCED_FACE('',(#2206),#8910,.T.);
#9194=ADVANCED_FACE('',(#2207),#413,.F.);
#9195=ADVANCED_FACE('',(#2208),#8911,.T.);
#9196=ADVANCED_FACE('',(#2209),#414,.F.);
#9197=ADVANCED_FACE('',(#2210),#8912,.T.);
#9198=ADVANCED_FACE('',(#2211),#415,.F.);
#9199=ADVANCED_FACE('',(#2212),#8913,.T.);
#9200=ADVANCED_FACE('',(#2213),#8914,.T.);
#9201=ADVANCED_FACE('',(#2214),#8915,.T.);
#9202=ADVANCED_FACE('',(#2215),#8916,.T.);
#9203=ADVANCED_FACE('',(#2216),#416,.T.);
#9204=ADVANCED_FACE('',(#2217),#417,.T.);
#9205=ADVANCED_FACE('',(#2218),#8917,.T.);
#9206=ADVANCED_FACE('',(#2219,#1981,#1982,#1983,#1984),#8918,.T.);
#9207=ADVANCED_FACE('',(#2220),#418,.T.);
#9208=ADVANCED_FACE('',(#2221),#419,.T.);
#9209=ADVANCED_FACE('',(#2222),#8919,.T.);
#9210=ADVANCED_FACE('',(#2223),#8920,.F.);
#9211=ADVANCED_FACE('',(#2224),#8921,.F.);
#9212=ADVANCED_FACE('',(#2225),#8922,.F.);
#9213=ADVANCED_FACE('',(#2226),#420,.T.);
#9214=ADVANCED_FACE('',(#2227),#8923,.T.);
#9215=ADVANCED_FACE('',(#2228,#1985,#1986,#1987,#1988),#8924,.T.);
#9216=ADVANCED_FACE('',(#2229),#421,.T.);
#9217=ADVANCED_FACE('',(#2230),#227,.T.);
#9218=ADVANCED_FACE('',(#2231),#228,.T.);
#9219=ADVANCED_FACE('',(#2232),#149,.T.);
#9220=ADVANCED_FACE('',(#2233),#150,.T.);
#9221=ADVANCED_FACE('',(#2234),#422,.T.);
#9222=ADVANCED_FACE('',(#2235),#151,.T.);
#9223=ADVANCED_FACE('',(#2236),#423,.T.);
#9224=ADVANCED_FACE('',(#2237),#424,.T.);
#9225=ADVANCED_FACE('',(#2238),#152,.T.);
#9226=ADVANCED_FACE('',(#2239),#425,.T.);
#9227=ADVANCED_FACE('',(#2240),#426,.T.);
#9228=ADVANCED_FACE('',(#2241),#229,.T.);
#9229=ADVANCED_FACE('',(#2242),#153,.T.);
#9230=ADVANCED_FACE('',(#2243),#230,.T.);
#9231=ADVANCED_FACE('',(#2244),#427,.T.);
#9232=ADVANCED_FACE('',(#2245),#428,.F.);
#9233=ADVANCED_FACE('',(#2246),#154,.T.);
#9234=ADVANCED_FACE('',(#2247),#231,.T.);
#9235=ADVANCED_FACE('',(#2248),#232,.T.);
#9236=ADVANCED_FACE('',(#2249),#429,.T.);
#9237=ADVANCED_FACE('',(#2250),#430,.F.);
#9238=ADVANCED_FACE('',(#2251),#155,.T.);
#9239=ADVANCED_FACE('',(#2252),#156,.T.);
#9240=ADVANCED_FACE('',(#2253),#431,.T.);
#9241=ADVANCED_FACE('',(#2254),#157,.T.);
#9242=ADVANCED_FACE('',(#2255),#432,.T.);
#9243=ADVANCED_FACE('',(#2256),#433,.T.);
#9244=ADVANCED_FACE('',(#2257),#158,.T.);
#9245=ADVANCED_FACE('',(#2258),#434,.T.);
#9246=ADVANCED_FACE('',(#2259),#435,.T.);
#9247=ADVANCED_FACE('',(#2260),#233,.T.);
#9248=ADVANCED_FACE('',(#2261),#159,.T.);
#9249=ADVANCED_FACE('',(#2262),#436,.T.);
#9250=ADVANCED_FACE('',(#2263),#234,.T.);
#9251=ADVANCED_FACE('',(#2264),#160,.T.);
#9252=ADVANCED_FACE('',(#2265),#437,.T.);
#9253=ADVANCED_FACE('',(#2266),#161,.T.);
#9254=ADVANCED_FACE('',(#2267),#438,.T.);
#9255=ADVANCED_FACE('',(#2268),#439,.T.);
#9256=ADVANCED_FACE('',(#2269),#162,.T.);
#9257=ADVANCED_FACE('',(#2270),#440,.T.);
#9258=ADVANCED_FACE('',(#2271),#441,.T.);
#9259=ADVANCED_FACE('',(#2272),#442,.T.);
#9260=ADVANCED_FACE('',(#2273),#443,.T.);
#9261=ADVANCED_FACE('',(#2274),#444,.T.);
#9262=ADVANCED_FACE('',(#2275),#445,.F.);
#9263=ADVANCED_FACE('',(#2276),#446,.T.);
#9264=ADVANCED_FACE('',(#2277),#447,.T.);
#9265=ADVANCED_FACE('',(#2278),#448,.T.);
#9266=ADVANCED_FACE('',(#2279),#449,.T.);
#9267=ADVANCED_FACE('',(#2280),#450,.T.);
#9268=ADVANCED_FACE('',(#2281),#451,.T.);
#9269=ADVANCED_FACE('',(#2282),#452,.T.);
#9270=ADVANCED_FACE('',(#2283),#453,.T.);
#9271=ADVANCED_FACE('',(#2284),#454,.F.);
#9272=ADVANCED_FACE('',(#2285),#8925,.F.);
#9273=ADVANCED_FACE('',(#2286),#8926,.F.);
#9274=ADVANCED_FACE('',(#2287),#8927,.F.);
#9275=ADVANCED_FACE('',(#2288),#8928,.F.);
#9276=ADVANCED_FACE('',(#2289),#8929,.F.);
#9277=ADVANCED_FACE('',(#2290),#8930,.F.);
#9278=ADVANCED_FACE('',(#2291),#8931,.F.);
#9279=ADVANCED_FACE('',(#2292),#8932,.T.);
#9280=ADVANCED_FACE('',(#2293),#8933,.F.);
#9281=ADVANCED_FACE('',(#2294),#8934,.T.);
#9282=ADVANCED_FACE('',(#2295),#8935,.T.);
#9631=CLOSED_SHELL('',(#9184,#9185,#9186,#9187,#9188,#9189,#9190,#9191,
#9192,#9193,#9194,#9195,#9196,#9197,#9198,#9199,#9200,#9201,#9202,#9203,
#9204,#9205,#9206,#9207,#9208,#9209,#9210,#9211,#9212,#9213,#9214,#9215,
#9216,#9217,#9218,#9219,#9220,#9221,#9222,#9223,#9224,#9225,#9226,#9227,
#9228,#9229,#9230,#9231,#9232,#9233,#9234,#9235,#9236,#9237,#9238,#9239,
#9240,#9241,#9242,#9243,#9244,#9245,#9246,#9247,#9248,#9249,#9250,#9251,
#9252,#9253,#9254,#9255,#9256,#9257,#9258,#9259,#9260,#9261,#9262,#9263,
#9264,#9265,#9266,#9267,#9268,#9269,#9270,#9271,#9272,#9273,#9274,#9275,
#9276,#9277,#9278,#9279,#9280,#9281,#9282));
#10101=AXIS2_PLACEMENT_3D('',#14990,#11915,#11916);
#10102=AXIS2_PLACEMENT_3D('',#14991,#11917,#11918);
#10103=AXIS2_PLACEMENT_3D('',#14993,#11919,#11920);
#10104=AXIS2_PLACEMENT_3D('',#14996,#11922,#11923);
#10105=AXIS2_PLACEMENT_3D('',#14997,#11924,#11925);
#10106=AXIS2_PLACEMENT_3D('',#14998,#11926,#11927);
#10107=AXIS2_PLACEMENT_3D('',#15000,#11928,#11929);
#10108=AXIS2_PLACEMENT_3D('',#15003,#11931,#11932);
#10109=AXIS2_PLACEMENT_3D('',#15004,#11933,#11934);
#10110=AXIS2_PLACEMENT_3D('',#15005,#11935,#11936);
#10111=AXIS2_PLACEMENT_3D('',#15007,#11937,#11938);
#10112=AXIS2_PLACEMENT_3D('',#15010,#11940,#11941);
#10113=AXIS2_PLACEMENT_3D('',#15011,#11942,#11943);
#10114=AXIS2_PLACEMENT_3D('',#15012,#11944,#11945);
#10115=AXIS2_PLACEMENT_3D('',#15014,#11946,#11947);
#10116=AXIS2_PLACEMENT_3D('',#15017,#11949,#11950);
#10117=AXIS2_PLACEMENT_3D('',#15018,#11951,#11952);
#10118=AXIS2_PLACEMENT_3D('',#15019,#11953,#11954);
#10119=AXIS2_PLACEMENT_3D('',#15021,#11955,#11956);
#10120=AXIS2_PLACEMENT_3D('',#15024,#11958,#11959);
#10121=AXIS2_PLACEMENT_3D('',#15025,#11960,#11961);
#10122=AXIS2_PLACEMENT_3D('',#15026,#11962,#11963);
#10123=AXIS2_PLACEMENT_3D('',#15028,#11964,#11965);
#10124=AXIS2_PLACEMENT_3D('',#15031,#11967,#11968);
#10125=AXIS2_PLACEMENT_3D('',#15032,#11969,#11970);
#10126=AXIS2_PLACEMENT_3D('',#15033,#11971,#11972);
#10127=AXIS2_PLACEMENT_3D('',#15035,#11973,#11974);
#10128=AXIS2_PLACEMENT_3D('',#15038,#11976,#11977);
#10129=AXIS2_PLACEMENT_3D('',#15039,#11978,#11979);
#10130=AXIS2_PLACEMENT_3D('',#15040,#11980,#11981);
#10131=AXIS2_PLACEMENT_3D('',#15042,#11982,#11983);
#10132=AXIS2_PLACEMENT_3D('',#15045,#11985,#11986);
#10133=AXIS2_PLACEMENT_3D('',#15046,#11987,#11988);
#10134=AXIS2_PLACEMENT_3D('',#15047,#11989,#11990);
#10135=AXIS2_PLACEMENT_3D('',#15050,#11991,#11992);
#10136=AXIS2_PLACEMENT_3D('',#15058,#11996,#11997);
#10137=AXIS2_PLACEMENT_3D('',#15060,#11999,#12000);
#10138=AXIS2_PLACEMENT_3D('',#15063,#12001,#12002);
#10139=AXIS2_PLACEMENT_3D('',#15067,#12004,#12005);
#10140=AXIS2_PLACEMENT_3D('',#15073,#12009,#12010);
#10141=AXIS2_PLACEMENT_3D('',#15076,#12013,#12014);
#10142=AXIS2_PLACEMENT_3D('',#15080,#12016,#12017);
#10143=AXIS2_PLACEMENT_3D('',#15082,#12019,#12020);
#10144=AXIS2_PLACEMENT_3D('',#15086,#12022,#12023);
#10145=AXIS2_PLACEMENT_3D('',#15088,#12025,#12026);
#10146=AXIS2_PLACEMENT_3D('',#15092,#12029,#12030);
#10147=AXIS2_PLACEMENT_3D('',#15096,#12033,#12034);
#10148=AXIS2_PLACEMENT_3D('',#15098,#12035,#12036);
#10149=AXIS2_PLACEMENT_3D('',#15100,#12038,#12039);
#10150=AXIS2_PLACEMENT_3D('',#15103,#12041,#12042);
#10151=AXIS2_PLACEMENT_3D('',#15104,#12043,#12044);
#10152=AXIS2_PLACEMENT_3D('',#15122,#12053,#12054);
#10153=AXIS2_PLACEMENT_3D('',#15128,#12057,#12058);
#10154=AXIS2_PLACEMENT_3D('',#15132,#12060,#12061);
#10155=AXIS2_PLACEMENT_3D('',#15138,#12064,#12065);
#10156=AXIS2_PLACEMENT_3D('',#15142,#12068,#12069);
#10157=AXIS2_PLACEMENT_3D('',#15144,#12070,#12071);
#10158=AXIS2_PLACEMENT_3D('',#15150,#12074,#12075);
#10159=AXIS2_PLACEMENT_3D('',#15152,#12077,#12078);
#10160=AXIS2_PLACEMENT_3D('',#15154,#12079,#12080);
#10161=AXIS2_PLACEMENT_3D('',#15158,#12082,#12083);
#10162=AXIS2_PLACEMENT_3D('',#15162,#12086,#12087);
#10163=AXIS2_PLACEMENT_3D('',#15164,#12089,#12090);
#10164=AXIS2_PLACEMENT_3D('',#15167,#12092,#12093);
#10165=AXIS2_PLACEMENT_3D('',#15168,#12094,#12095);
#10166=AXIS2_PLACEMENT_3D('',#15174,#12098,#12099);
#10167=AXIS2_PLACEMENT_3D('',#15180,#12102,#12103);
#10168=AXIS2_PLACEMENT_3D('',#15184,#12105,#12106);
#10169=AXIS2_PLACEMENT_3D('',#15190,#12109,#12110);
#10170=AXIS2_PLACEMENT_3D('',#15199,#12116,#12117);
#10171=AXIS2_PLACEMENT_3D('',#15203,#12120,#12121);
#10172=AXIS2_PLACEMENT_3D('',#15206,#12123,#12124);
#10173=AXIS2_PLACEMENT_3D('',#15207,#12125,#12126);
#10174=AXIS2_PLACEMENT_3D('',#15209,#12127,#12128);
#10175=AXIS2_PLACEMENT_3D('',#15211,#12129,#12130);
#10176=AXIS2_PLACEMENT_3D('',#15212,#12131,#12132);
#10177=AXIS2_PLACEMENT_3D('',#15213,#12133,#12134);
#10178=AXIS2_PLACEMENT_3D('',#15215,#12135,#12136);
#10179=AXIS2_PLACEMENT_3D('',#15217,#12137,#12138);
#10180=AXIS2_PLACEMENT_3D('',#15218,#12139,#12140);
#10181=AXIS2_PLACEMENT_3D('',#15219,#12141,#12142);
#10182=AXIS2_PLACEMENT_3D('',#15221,#12143,#12144);
#10183=AXIS2_PLACEMENT_3D('',#15223,#12145,#12146);
#10184=AXIS2_PLACEMENT_3D('',#15224,#12147,#12148);
#10185=AXIS2_PLACEMENT_3D('',#15225,#12149,#12150);
#10186=AXIS2_PLACEMENT_3D('',#15227,#12151,#12152);
#10187=AXIS2_PLACEMENT_3D('',#15229,#12153,#12154);
#10188=AXIS2_PLACEMENT_3D('',#15230,#12155,#12156);
#10189=AXIS2_PLACEMENT_3D('',#15231,#12157,#12158);
#10190=AXIS2_PLACEMENT_3D('',#15233,#12160,#12161);
#10191=AXIS2_PLACEMENT_3D('',#15235,#12162,#12163);
#10192=AXIS2_PLACEMENT_3D('',#15237,#12164,#12165);
#10193=AXIS2_PLACEMENT_3D('',#15238,#12166,#12167);
#10194=AXIS2_PLACEMENT_3D('',#15239,#12168,#12169);
#10195=AXIS2_PLACEMENT_3D('',#15241,#12171,#12172);
#10196=AXIS2_PLACEMENT_3D('',#15244,#12175,#12176);
#10197=AXIS2_PLACEMENT_3D('',#15246,#12177,#12178);
#10198=AXIS2_PLACEMENT_3D('',#15248,#12179,#12180);
#10199=AXIS2_PLACEMENT_3D('',#15249,#12181,#12182);
#10200=AXIS2_PLACEMENT_3D('',#15250,#12183,#12184);
#10201=AXIS2_PLACEMENT_3D('',#15253,#12187,#12188);
#10202=AXIS2_PLACEMENT_3D('',#15255,#12190,#12191);
#10203=AXIS2_PLACEMENT_3D('',#15257,#12192,#12193);
#10204=AXIS2_PLACEMENT_3D('',#15259,#12194,#12195);
#10205=AXIS2_PLACEMENT_3D('',#15260,#12196,#12197);
#10206=AXIS2_PLACEMENT_3D('',#15261,#12198,#12199);
#10207=AXIS2_PLACEMENT_3D('',#15263,#12200,#12201);
#10208=AXIS2_PLACEMENT_3D('',#15264,#12202,#12203);
#10209=AXIS2_PLACEMENT_3D('',#15265,#12204,#12205);
#10210=AXIS2_PLACEMENT_3D('',#15267,#12206,#12207);
#10211=AXIS2_PLACEMENT_3D('',#15269,#12208,#12209);
#10212=AXIS2_PLACEMENT_3D('',#15270,#12210,#12211);
#10213=AXIS2_PLACEMENT_3D('',#15271,#12212,#12213);
#10214=AXIS2_PLACEMENT_3D('',#15273,#12215,#12216);
#10215=AXIS2_PLACEMENT_3D('',#15276,#12219,#12220);
#10216=AXIS2_PLACEMENT_3D('',#15278,#12221,#12222);
#10217=AXIS2_PLACEMENT_3D('',#15279,#12223,#12224);
#10218=AXIS2_PLACEMENT_3D('',#15280,#12225,#12226);
#10219=AXIS2_PLACEMENT_3D('',#15282,#12227,#12228);
#10220=AXIS2_PLACEMENT_3D('',#15284,#12229,#12230);
#10221=AXIS2_PLACEMENT_3D('',#15285,#12231,#12232);
#10222=AXIS2_PLACEMENT_3D('',#15286,#12233,#12234);
#10223=AXIS2_PLACEMENT_3D('',#15288,#12235,#12236);
#10224=AXIS2_PLACEMENT_3D('',#15290,#12237,#12238);
#10225=AXIS2_PLACEMENT_3D('',#15291,#12239,#12240);
#10226=AXIS2_PLACEMENT_3D('',#15292,#12241,#12242);
#10227=AXIS2_PLACEMENT_3D('',#15294,#12244,#12245);
#10228=AXIS2_PLACEMENT_3D('',#15297,#12248,#12249);
#10229=AXIS2_PLACEMENT_3D('',#15299,#12250,#12251);
#10230=AXIS2_PLACEMENT_3D('',#15301,#12252,#12253);
#10231=AXIS2_PLACEMENT_3D('',#15302,#12254,#12255);
#10232=AXIS2_PLACEMENT_3D('',#15303,#12256,#12257);
#10233=AXIS2_PLACEMENT_3D('',#15305,#12258,#12259);
#10234=AXIS2_PLACEMENT_3D('',#15307,#12260,#12261);
#10235=AXIS2_PLACEMENT_3D('',#15308,#12262,#12263);
#10236=AXIS2_PLACEMENT_3D('',#15309,#12264,#12265);
#10237=AXIS2_PLACEMENT_3D('',#15311,#12267,#12268);
#10238=AXIS2_PLACEMENT_3D('',#15313,#12269,#12270);
#10239=AXIS2_PLACEMENT_3D('',#15315,#12271,#12272);
#10240=AXIS2_PLACEMENT_3D('',#15316,#12273,#12274);
#10241=AXIS2_PLACEMENT_3D('',#15317,#12275,#12276);
#10242=AXIS2_PLACEMENT_3D('',#15319,#12278,#12279);
#10243=AXIS2_PLACEMENT_3D('',#15322,#12282,#12283);
#10244=AXIS2_PLACEMENT_3D('',#15324,#12284,#12285);
#10245=AXIS2_PLACEMENT_3D('',#15325,#12286,#12287);
#10246=AXIS2_PLACEMENT_3D('',#15326,#12288,#12289);
#10247=AXIS2_PLACEMENT_3D('',#15329,#12292,#12293);
#10248=AXIS2_PLACEMENT_3D('',#15331,#12295,#12296);
#10249=AXIS2_PLACEMENT_3D('',#15333,#12297,#12298);
#10250=AXIS2_PLACEMENT_3D('',#15335,#12299,#12300);
#10251=AXIS2_PLACEMENT_3D('',#15336,#12301,#12302);
#10252=AXIS2_PLACEMENT_3D('',#15337,#12303,#12304);
#10253=AXIS2_PLACEMENT_3D('',#15339,#12305,#12306);
#10254=AXIS2_PLACEMENT_3D('',#15340,#12307,#12308);
#10255=AXIS2_PLACEMENT_3D('',#15341,#12309,#12310);
#10256=AXIS2_PLACEMENT_3D('',#15343,#12312,#12313);
#10257=AXIS2_PLACEMENT_3D('',#15345,#12314,#12315);
#10258=AXIS2_PLACEMENT_3D('',#15347,#12316,#12317);
#10259=AXIS2_PLACEMENT_3D('',#15348,#12318,#12319);
#10260=AXIS2_PLACEMENT_3D('',#15349,#12320,#12321);
#10261=AXIS2_PLACEMENT_3D('',#15351,#12322,#12323);
#10262=AXIS2_PLACEMENT_3D('',#15352,#12324,#12325);
#10263=AXIS2_PLACEMENT_3D('',#15353,#12326,#12327);
#10264=AXIS2_PLACEMENT_3D('',#15354,#12328,#12329);
#10265=AXIS2_PLACEMENT_3D('',#15355,#12330,#12331);
#10266=AXIS2_PLACEMENT_3D('',#15358,#12332,#12333);
#10267=AXIS2_PLACEMENT_3D('',#15359,#12334,#12335);
#10268=AXIS2_PLACEMENT_3D('',#15360,#12336,#12337);
#10269=AXIS2_PLACEMENT_3D('',#15361,#12338,#12339);
#10270=AXIS2_PLACEMENT_3D('',#15363,#12341,#12342);
#10271=AXIS2_PLACEMENT_3D('',#15365,#12344,#12345);
#10272=AXIS2_PLACEMENT_3D('',#15367,#12346,#12347);
#10273=AXIS2_PLACEMENT_3D('',#15369,#12348,#12349);
#10274=AXIS2_PLACEMENT_3D('',#15370,#12350,#12351);
#10275=AXIS2_PLACEMENT_3D('',#15371,#12352,#12353);
#10276=AXIS2_PLACEMENT_3D('',#15374,#12356,#12357);
#10277=AXIS2_PLACEMENT_3D('',#15376,#12359,#12360);
#10278=AXIS2_PLACEMENT_3D('',#15378,#12362,#12363);
#10279=AXIS2_PLACEMENT_3D('',#15380,#12365,#12366);
#10280=AXIS2_PLACEMENT_3D('',#15382,#12368,#12369);
#10281=AXIS2_PLACEMENT_3D('',#15385,#12372,#12373);
#10282=AXIS2_PLACEMENT_3D('',#15387,#12375,#12376);
#10283=AXIS2_PLACEMENT_3D('',#15389,#12378,#12379);
#10284=AXIS2_PLACEMENT_3D('',#15391,#12381,#12382);
#10285=AXIS2_PLACEMENT_3D('',#15393,#12384,#12385);
#10286=AXIS2_PLACEMENT_3D('',#15395,#12387,#12388);
#10287=AXIS2_PLACEMENT_3D('',#15397,#12390,#12391);
#10288=AXIS2_PLACEMENT_3D('',#15399,#12393,#12394);
#10289=AXIS2_PLACEMENT_3D('',#15401,#12396,#12397);
#10290=AXIS2_PLACEMENT_3D('',#15404,#12400,#12401);
#10291=AXIS2_PLACEMENT_3D('',#15405,#12402,#12403);
#10292=AXIS2_PLACEMENT_3D('',#15406,#12404,#12405);
#10293=AXIS2_PLACEMENT_3D('',#15407,#12406,#12407);
#10294=AXIS2_PLACEMENT_3D('',#15408,#12408,#12409);
#10295=AXIS2_PLACEMENT_3D('',#15409,#12410,#12411);
#10296=AXIS2_PLACEMENT_3D('',#15410,#12412,#12413);
#10297=AXIS2_PLACEMENT_3D('',#15411,#12414,#12415);
#10298=AXIS2_PLACEMENT_3D('',#15412,#12416,#12417);
#10299=AXIS2_PLACEMENT_3D('',#15413,#12418,#12419);
#10300=AXIS2_PLACEMENT_3D('',#15414,#12420,#12421);
#11915=DIRECTION('axis',(0.,0.,1.));
#11916=DIRECTION('refdir',(1.,0.,0.));
#11917=DIRECTION('center_axis',(0.,1.,0.));
#11918=DIRECTION('ref_axis',(1.,0.,0.));
#11919=DIRECTION('center_axis',(-2.22044604925031E-16,-1.,0.));
#11920=DIRECTION('ref_axis',(1.,0.,0.));
#11921=DIRECTION('',(0.,-1.,0.));
#11922=DIRECTION('center_axis',(0.,1.,0.));
#11923=DIRECTION('ref_axis',(1.,0.,0.));
#11924=DIRECTION('center_axis',(0.,-1.,0.));
#11925=DIRECTION('ref_axis',(1.,0.,0.));
#11926=DIRECTION('center_axis',(0.,1.,0.));
#11927=DIRECTION('ref_axis',(1.,0.,0.));
#11928=DIRECTION('center_axis',(-2.22044604925031E-16,-1.,0.));
#11929=DIRECTION('ref_axis',(1.,0.,0.));
#11930=DIRECTION('',(0.,-1.,0.));
#11931=DIRECTION('center_axis',(0.,1.,0.));
#11932=DIRECTION('ref_axis',(1.,0.,0.));
#11933=DIRECTION('center_axis',(0.,-1.,0.));
#11934=DIRECTION('ref_axis',(1.,0.,0.));
#11935=DIRECTION('center_axis',(0.,1.,0.));
#11936=DIRECTION('ref_axis',(1.,0.,0.));
#11937=DIRECTION('center_axis',(-2.22044604925031E-16,-1.,0.));
#11938=DIRECTION('ref_axis',(1.,0.,0.));
#11939=DIRECTION('',(0.,-1.,0.));
#11940=DIRECTION('center_axis',(0.,1.,0.));
#11941=DIRECTION('ref_axis',(1.,0.,0.));
#11942=DIRECTION('center_axis',(0.,-1.,0.));
#11943=DIRECTION('ref_axis',(1.,0.,0.));
#11944=DIRECTION('center_axis',(0.,1.,0.));
#11945=DIRECTION('ref_axis',(1.,0.,0.));
#11946=DIRECTION('center_axis',(-2.22044604925031E-16,-1.,0.));
#11947=DIRECTION('ref_axis',(1.,0.,0.));
#11948=DIRECTION('',(0.,-1.,0.));
#11949=DIRECTION('center_axis',(0.,1.,0.));
#11950=DIRECTION('ref_axis',(1.,0.,0.));
#11951=DIRECTION('center_axis',(0.,-1.,0.));
#11952=DIRECTION('ref_axis',(1.,0.,0.));
#11953=DIRECTION('center_axis',(0.,1.,0.));
#11954=DIRECTION('ref_axis',(1.,0.,0.));
#11955=DIRECTION('center_axis',(2.22044604925031E-16,1.,0.));
#11956=DIRECTION('ref_axis',(1.,0.,0.));
#11957=DIRECTION('',(0.,1.,0.));
#11958=DIRECTION('center_axis',(0.,1.,0.));
#11959=DIRECTION('ref_axis',(1.,0.,0.));
#11960=DIRECTION('center_axis',(0.,-1.,0.));
#11961=DIRECTION('ref_axis',(1.,0.,0.));
#11962=DIRECTION('center_axis',(0.,1.,0.));
#11963=DIRECTION('ref_axis',(1.,0.,0.));
#11964=DIRECTION('center_axis',(2.22044604925031E-16,1.,0.));
#11965=DIRECTION('ref_axis',(1.,0.,0.));
#11966=DIRECTION('',(0.,1.,0.));
#11967=DIRECTION('center_axis',(0.,1.,0.));
#11968=DIRECTION('ref_axis',(1.,0.,0.));
#11969=DIRECTION('center_axis',(0.,-1.,0.));
#11970=DIRECTION('ref_axis',(1.,0.,0.));
#11971=DIRECTION('center_axis',(0.,1.,0.));
#11972=DIRECTION('ref_axis',(1.,0.,0.));
#11973=DIRECTION('center_axis',(2.22044604925031E-16,1.,0.));
#11974=DIRECTION('ref_axis',(1.,0.,0.));
#11975=DIRECTION('',(0.,1.,0.));
#11976=DIRECTION('center_axis',(0.,1.,0.));
#11977=DIRECTION('ref_axis',(1.,0.,0.));
#11978=DIRECTION('center_axis',(0.,-1.,0.));
#11979=DIRECTION('ref_axis',(1.,0.,0.));
#11980=DIRECTION('center_axis',(0.,1.,0.));
#11981=DIRECTION('ref_axis',(1.,0.,0.));
#11982=DIRECTION('center_axis',(2.22044604925031E-16,1.,0.));
#11983=DIRECTION('ref_axis',(1.,0.,0.));
#11984=DIRECTION('',(0.,1.,0.));
#11985=DIRECTION('center_axis',(0.,1.,0.));
#11986=DIRECTION('ref_axis',(1.,0.,0.));
#11987=DIRECTION('center_axis',(0.,-1.,0.));
#11988=DIRECTION('ref_axis',(1.,0.,0.));
#11989=DIRECTION('center_axis',(0.,0.,-1.));
#11990=DIRECTION('ref_axis',(2.22044604925031E-16,1.,0.));
#11991=DIRECTION('center_axis',(0.,0.,1.));
#11992=DIRECTION('ref_axis',(-0.707106781186548,-0.707106781186547,0.));
#11993=DIRECTION('',(-2.22044604925031E-16,-1.,0.));
#11994=DIRECTION('',(1.,-2.22044604925031E-16,0.));
#11995=DIRECTION('',(2.22044604925031E-16,1.,0.));
#11996=DIRECTION('center_axis',(0.,0.,1.));
#11997=DIRECTION('ref_axis',(0.707106781186547,-0.707106781186548,0.));
#11998=DIRECTION('',(1.,-2.22044604925031E-16,0.));
#11999=DIRECTION('center_axis',(0.,0.,1.));
#12000=DIRECTION('ref_axis',(-2.22044604925031E-16,-1.,0.));
#12001=DIRECTION('center_axis',(0.,0.,-1.));
#12002=DIRECTION('ref_axis',(-0.707106781186548,-0.707106781186547,0.));
#12003=DIRECTION('',(-1.,2.22044604925031E-16,0.));
#12004=DIRECTION('center_axis',(0.,0.,-1.));
#12005=DIRECTION('ref_axis',(0.707106781186547,-0.707106781186548,0.));
#12006=DIRECTION('',(-2.22044604925031E-16,-1.,0.));
#12007=DIRECTION('',(1.,-2.22044604925031E-16,0.));
#12008=DIRECTION('',(2.22044604925031E-16,1.,0.));
#12009=DIRECTION('center_axis',(-2.22044604925031E-16,-1.,0.));
#12010=DIRECTION('ref_axis',(0.,0.,-1.));
#12011=DIRECTION('',(0.,0.,-1.));
#12012=DIRECTION('',(0.,0.,1.));
#12013=DIRECTION('center_axis',(0.,0.,1.));
#12014=DIRECTION('ref_axis',(-0.707106781186548,-0.707106781186547,0.));
#12015=DIRECTION('',(0.,0.,-1.));
#12016=DIRECTION('center_axis',(-1.57009245868376E-16,-0.707106781186543,
0.707106781186553));
#12017=DIRECTION('ref_axis',(-1.57009245868379E-16,-0.707106781186553,-0.707106781186543));
#12018=DIRECTION('',(0.,0.,1.));
#12019=DIRECTION('center_axis',(0.,0.,1.));
#12020=DIRECTION('ref_axis',(-0.707106781186548,-0.707106781186547,0.));
#12021=DIRECTION('',(0.,0.,1.));
#12022=DIRECTION('center_axis',(0.,0.,1.));
#12023=DIRECTION('ref_axis',(-2.22044604925031E-16,-1.,0.));
#12024=DIRECTION('',(0.,0.,-1.));
#12025=DIRECTION('center_axis',(-2.22044604925031E-16,-1.,0.));
#12026=DIRECTION('ref_axis',(1.,-2.22044604925031E-16,0.));
#12027=DIRECTION('',(1.,-2.22044604925031E-16,0.));
#12028=DIRECTION('',(0.,0.,-1.));
#12029=DIRECTION('center_axis',(-2.22044604925031E-16,-1.,0.));
#12030=DIRECTION('ref_axis',(1.,-2.22044604925031E-16,0.));
#12031=DIRECTION('',(0.,0.,-1.));
#12032=DIRECTION('',(1.,-2.22044604925031E-16,0.));
#12033=DIRECTION('center_axis',(0.,0.,1.));
#12034=DIRECTION('ref_axis',(0.707106781186547,-0.707106781186548,0.));
#12035=DIRECTION('center_axis',(1.57009245868376E-16,0.707106781186543,
-0.707106781186553));
#12036=DIRECTION('ref_axis',(-1.57009245868379E-16,-0.707106781186553,-0.707106781186542));
#12037=DIRECTION('',(0.,0.,1.));
#12038=DIRECTION('center_axis',(0.,0.,1.));
#12039=DIRECTION('ref_axis',(0.707106781186547,-0.707106781186548,0.));
#12040=DIRECTION('',(0.,0.,1.));
#12041=DIRECTION('center_axis',(0.,0.,1.));
#12042=DIRECTION('ref_axis',(1.,-2.22044604925031E-16,0.));
#12043=DIRECTION('center_axis',(1.,-2.22044604925031E-16,0.));
#12044=DIRECTION('ref_axis',(2.22044604925031E-16,1.,0.));
#12045=DIRECTION('',(-2.22044604925031E-16,-1.,0.));
#12046=DIRECTION('',(0.,0.,-1.));
#12047=DIRECTION('',(-2.22044604925031E-16,-1.,0.));
#12048=DIRECTION('',(0.,0.,1.));
#12049=DIRECTION('',(2.22044604925031E-16,1.,0.));
#12050=DIRECTION('',(0.,0.,-1.));
#12051=DIRECTION('',(2.22044604925031E-16,1.,0.));
#12052=DIRECTION('',(-1.57009245868377E-16,-0.707106781186548,0.707106781186548));
#12053=DIRECTION('center_axis',(1.,-2.22044604925031E-16,0.));
#12054=DIRECTION('ref_axis',(2.05142465794796E-16,0.923879532511307,-0.38268343236504));
#12055=DIRECTION('',(2.22044604925031E-16,1.,0.));
#12056=DIRECTION('',(0.,0.,1.));
#12057=DIRECTION('center_axis',(1.,-2.22044604925031E-16,0.));
#12058=DIRECTION('ref_axis',(1.57009245868378E-16,0.70710678118655,-0.707106781186544));
#12059=DIRECTION('',(2.22044604925031E-16,1.,0.));
#12060=DIRECTION('center_axis',(1.,-2.22044604925031E-16,0.));
#12061=DIRECTION('ref_axis',(-1.57009245868377E-16,-0.707106781186546,-0.707106781186549));
#12062=DIRECTION('',(0.,0.,-1.));
#12063=DIRECTION('',(2.22044604925031E-16,1.,0.));
#12064=DIRECTION('center_axis',(1.,-2.22044604925031E-16,0.));
#12065=DIRECTION('ref_axis',(-1.57009245868377E-16,-0.707106781186546,-0.707106781186549));
#12066=DIRECTION('',(0.,0.,-1.));
#12067=DIRECTION('',(2.22044604925031E-16,1.,0.));
#12068=DIRECTION('center_axis',(0.,0.,1.));
#12069=DIRECTION('ref_axis',(-2.22044604925031E-16,-1.,0.));
#12070=DIRECTION('center_axis',(0.,0.,1.));
#12071=DIRECTION('ref_axis',(0.707106781186548,0.707106781186547,0.));
#12072=DIRECTION('',(1.,-2.22044604925031E-16,0.));
#12073=DIRECTION('',(-2.22044604925031E-16,-1.,0.));
#12074=DIRECTION('center_axis',(0.,0.,1.));
#12075=DIRECTION('ref_axis',(-0.707106781186547,0.707106781186548,0.));
#12076=DIRECTION('',(-1.,2.22044604925031E-16,0.));
#12077=DIRECTION('center_axis',(0.,0.,-1.));
#12078=DIRECTION('ref_axis',(2.22044604925031E-16,1.,0.));
#12079=DIRECTION('center_axis',(0.,0.,-1.));
#12080=DIRECTION('ref_axis',(0.707106781186548,0.707106781186547,0.));
#12081=DIRECTION('',(1.,-2.22044604925031E-16,0.));
#12082=DIRECTION('center_axis',(0.,0.,-1.));
#12083=DIRECTION('ref_axis',(-0.707106781186547,0.707106781186548,0.));
#12084=DIRECTION('',(2.22044604925031E-16,1.,0.));
#12085=DIRECTION('',(1.,-2.22044604925031E-16,0.));
#12086=DIRECTION('center_axis',(-2.22044604925031E-16,-1.,0.));
#12087=DIRECTION('ref_axis',(0.,0.,-1.));
#12088=DIRECTION('',(0.,0.,-1.));
#12089=DIRECTION('center_axis',(0.,0.,1.));
#12090=DIRECTION('ref_axis',(0.707106781186548,0.707106781186547,0.));
#12091=DIRECTION('',(0.,0.,1.));
#12092=DIRECTION('center_axis',(0.,0.,1.));
#12093=DIRECTION('ref_axis',(2.22044604925031E-16,1.,0.));
#12094=DIRECTION('center_axis',(-1.,2.22044604925031E-16,0.));
#12095=DIRECTION('ref_axis',(-2.22044604925031E-16,-1.,0.));
#12096=DIRECTION('',(-2.22044604925031E-16,-1.,0.));
#12097=DIRECTION('',(0.,0.,1.));
#12098=DIRECTION('center_axis',(-1.,2.22044604925031E-16,0.));
#12099=DIRECTION('ref_axis',(-1.57009245868379E-16,-0.707106781186552,-0.707106781186543));
#12100=DIRECTION('',(-2.22044604925031E-16,-1.,0.));
#12101=DIRECTION('',(0.,0.,1.));
#12102=DIRECTION('center_axis',(-1.,2.22044604925031E-16,0.));
#12103=DIRECTION('ref_axis',(-1.57009245868377E-16,-0.707106781186546,-0.707106781186549));
#12104=DIRECTION('',(-2.22044604925031E-16,-1.,0.));
#12105=DIRECTION('center_axis',(-1.,2.22044604925031E-16,0.));
#12106=DIRECTION('ref_axis',(1.57009245868377E-16,0.707106781186547,-0.707106781186547));
#12107=DIRECTION('',(0.,0.,-1.));
#12108=DIRECTION('',(-2.22044604925031E-16,-1.,0.));
#12109=DIRECTION('center_axis',(-1.,2.22044604925031E-16,0.));
#12110=DIRECTION('ref_axis',(2.0514246579479E-16,0.923879532511279,-0.382683432365108));
#12111=DIRECTION('',(1.57009245868377E-16,0.707106781186548,-0.707106781186548));
#12112=DIRECTION('',(-2.22044604925031E-16,-1.,0.));
#12113=DIRECTION('',(0.,0.,1.));
#12114=DIRECTION('',(0.,0.,1.));
#12115=DIRECTION('',(2.22044604925031E-16,1.,0.));
#12116=DIRECTION('center_axis',(2.22044604925031E-16,1.,0.));
#12117=DIRECTION('ref_axis',(-1.,2.22044604925031E-16,0.));
#12118=DIRECTION('',(0.,0.,-1.));
#12119=DIRECTION('',(-1.,2.22044604925031E-16,0.));
#12120=DIRECTION('center_axis',(0.,0.,1.));
#12121=DIRECTION('ref_axis',(-0.707106781186547,0.707106781186548,0.));
#12122=DIRECTION('',(0.,0.,-1.));
#12123=DIRECTION('center_axis',(0.,0.,-1.));
#12124=DIRECTION('ref_axis',(2.22044604925031E-16,1.,0.));
#12125=DIRECTION('center_axis',(1.,-2.22044604925031E-16,0.));
#12126=DIRECTION('ref_axis',(0.,0.,1.));
#12127=DIRECTION('center_axis',(2.22044604925031E-16,1.,0.));
#12128=DIRECTION('ref_axis',(0.,0.,1.));
#12129=DIRECTION('center_axis',(-1.,2.22044604925031E-16,0.));
#12130=DIRECTION('ref_axis',(-2.22044604925031E-16,-1.,0.));
#12131=DIRECTION('center_axis',(0.,0.,1.));
#12132=DIRECTION('ref_axis',(1.,-2.22044604925031E-16,0.));
#12133=DIRECTION('center_axis',(-1.,2.22044604925031E-16,0.));
#12134=DIRECTION('ref_axis',(0.,0.,-1.));
#12135=DIRECTION('center_axis',(0.,0.,1.));
#12136=DIRECTION('ref_axis',(2.22044604925031E-16,1.,0.));
#12137=DIRECTION('center_axis',(1.,-2.22044604925031E-16,0.));
#12138=DIRECTION('ref_axis',(0.,0.,-1.));
#12139=DIRECTION('center_axis',(2.22044604925031E-16,1.,0.));
#12140=DIRECTION('ref_axis',(-1.,2.22044604925031E-16,0.));
#12141=DIRECTION('center_axis',(-0.408248290463861,0.816496580927728,-0.408248290463861));
#12142=DIRECTION('ref_axis',(0.577350269189626,0.577350269189626,0.577350269189626));
#12143=DIRECTION('center_axis',(2.22044604925031E-16,1.,0.));
#12144=DIRECTION('ref_axis',(1.,-2.22044604925031E-16,0.));
#12145=DIRECTION('center_axis',(0.,0.,1.));
#12146=DIRECTION('ref_axis',(2.22044604925031E-16,1.,0.));
#12147=DIRECTION('center_axis',(1.,-2.22044604925031E-16,0.));
#12148=DIRECTION('ref_axis',(0.,0.,1.));
#12149=DIRECTION('center_axis',(-0.408248290463863,0.816496580927726,-0.408248290463863));
#12150=DIRECTION('ref_axis',(0.577350269189626,0.577350269189626,0.577350269189626));
#12151=DIRECTION('center_axis',(2.22044604925031E-16,1.,0.));
#12152=DIRECTION('ref_axis',(1.,-2.22044604925031E-16,0.));
#12153=DIRECTION('center_axis',(4.44089209850056E-15,-9.86076131526251E-31,
1.));
#12154=DIRECTION('ref_axis',(2.22044604925031E-16,1.,0.));
#12155=DIRECTION('center_axis',(1.,-2.22044604925031E-16,0.));
#12156=DIRECTION('ref_axis',(0.,0.,1.));
#12157=DIRECTION('center_axis',(0.,0.,1.));
#12158=DIRECTION('ref_axis',(0.70710678118656,0.707106781186535,0.));
#12159=DIRECTION('',(0.,0.,1.));
#12160=DIRECTION('center_axis',(0.408248290463861,0.816496580927728,-0.408248290463861));
#12161=DIRECTION('ref_axis',(-0.577350269189623,0.577350269189631,0.577350269189623));
#12162=DIRECTION('center_axis',(0.,0.,1.));
#12163=DIRECTION('ref_axis',(-1.,2.22044604925031E-16,0.));
#12164=DIRECTION('center_axis',(2.22044604925031E-16,1.,0.));
#12165=DIRECTION('ref_axis',(0.,0.,1.));
#12166=DIRECTION('center_axis',(-1.,2.22044604925031E-16,0.));
#12167=DIRECTION('ref_axis',(2.22044604925031E-16,1.,0.));
#12168=DIRECTION('center_axis',(2.22044604925031E-16,1.,0.));
#12169=DIRECTION('ref_axis',(-0.707106781186551,1.57009245868378E-16,0.707106781186544));
#12170=DIRECTION('',(2.22044604925031E-16,1.,0.));
#12171=DIRECTION('center_axis',(-1.,2.22044604925031E-16,0.));
#12172=DIRECTION('ref_axis',(1.57009245868377E-16,0.707106781186544,0.707106781186551));
#12173=DIRECTION('',(1.,-2.22044604925031E-16,0.));
#12174=DIRECTION('',(-1.,2.22044604925031E-16,0.));
#12175=DIRECTION('center_axis',(0.408248290463861,0.816496580927736,-0.408248290463846));
#12176=DIRECTION('ref_axis',(-0.577350269189631,0.577350269189616,0.577350269189631));
#12177=DIRECTION('center_axis',(-1.75415237890772E-14,1.,0.));
#12178=DIRECTION('ref_axis',(0.,0.,1.));
#12179=DIRECTION('center_axis',(-1.,2.22044604925031E-16,0.));
#12180=DIRECTION('ref_axis',(2.22044604925031E-16,1.,0.));
#12181=DIRECTION('center_axis',(-9.86076131526251E-31,-4.44089209850056E-15,
1.));
#12182=DIRECTION('ref_axis',(-1.,2.22044604925031E-16,0.));
#12183=DIRECTION('center_axis',(-1.,2.22044604925031E-16,0.));
#12184=DIRECTION('ref_axis',(1.57009245868376E-16,0.707106781186541,0.707106781186554));
#12185=DIRECTION('',(1.,-2.22044604925031E-16,0.));
#12186=DIRECTION('',(-1.,2.22044604925031E-16,0.));
#12187=DIRECTION('center_axis',(0.,0.,-1.));
#12188=DIRECTION('ref_axis',(-0.707106781186547,0.707106781186548,0.));
#12189=DIRECTION('',(0.,0.,-1.));
#12190=DIRECTION('center_axis',(1.,-2.22044604925031E-16,0.));
#12191=DIRECTION('ref_axis',(0.,0.,1.));
#12192=DIRECTION('center_axis',(2.22044604925031E-16,1.,0.));
#12193=DIRECTION('ref_axis',(0.,0.,1.));
#12194=DIRECTION('center_axis',(-1.,2.22044604925031E-16,0.));
#12195=DIRECTION('ref_axis',(-2.22044604925031E-16,-1.,0.));
#12196=DIRECTION('center_axis',(0.,0.,1.));
#12197=DIRECTION('ref_axis',(1.,-2.22044604925031E-16,0.));
#12198=DIRECTION('center_axis',(0.408248290463854,-0.408248290463854,-0.816496580927736));
#12199=DIRECTION('ref_axis',(0.577350269189616,-0.577350269189645,0.577350269189616));
#12200=DIRECTION('center_axis',(1.,-2.22044604925031E-16,0.));
#12201=DIRECTION('ref_axis',(-2.22044604925031E-16,-1.,0.));
#12202=DIRECTION('center_axis',(1.75415237890772E-14,-1.,0.));
#12203=DIRECTION('ref_axis',(0.,0.,1.));
#12204=DIRECTION('center_axis',(-1.,2.22044604925031E-16,0.));
#12205=DIRECTION('ref_axis',(0.,0.,-1.));
#12206=DIRECTION('center_axis',(0.,0.,1.));
#12207=DIRECTION('ref_axis',(2.22044604925031E-16,1.,0.));
#12208=DIRECTION('center_axis',(1.,-2.22044604925031E-16,0.));
#12209=DIRECTION('ref_axis',(0.,0.,-1.));
#12210=DIRECTION('center_axis',(2.22044604925031E-16,1.,0.));
#12211=DIRECTION('ref_axis',(-1.,2.22044604925031E-16,0.));
#12212=DIRECTION('center_axis',(0.,0.,-1.));
#12213=DIRECTION('ref_axis',(-0.707106781186554,0.707106781186541,0.));
#12214=DIRECTION('',(0.,0.,-1.));
#12215=DIRECTION('center_axis',(-1.,2.22044604925031E-16,0.));
#12216=DIRECTION('ref_axis',(-1.57009245868377E-16,-0.707106781186547,-0.707106781186548));
#12217=DIRECTION('',(1.,-2.22044604925031E-16,0.));
#12218=DIRECTION('',(-1.,2.22044604925031E-16,0.));
#12219=DIRECTION('center_axis',(-0.408248290463851,0.816496580927731,0.408248290463865));
#12220=DIRECTION('ref_axis',(-0.577350269189626,-0.577350269189626,0.577350269189626));
#12221=DIRECTION('center_axis',(-2.22044604925031E-16,-1.,0.));
#12222=DIRECTION('ref_axis',(-1.,2.22044604925031E-16,0.));
#12223=DIRECTION('center_axis',(-1.,2.22044604925031E-16,0.));
#12224=DIRECTION('ref_axis',(0.,0.,1.));
#12225=DIRECTION('center_axis',(1.,-2.22044604925031E-16,0.));
#12226=DIRECTION('ref_axis',(0.,0.,1.));
#12227=DIRECTION('center_axis',(0.,0.,1.));
#12228=DIRECTION('ref_axis',(-2.22044604925031E-16,-1.,0.));
#12229=DIRECTION('center_axis',(-1.,2.22044604925031E-16,0.));
#12230=DIRECTION('ref_axis',(0.,0.,-1.));
#12231=DIRECTION('center_axis',(-2.22044604925031E-16,-1.,0.));
#12232=DIRECTION('ref_axis',(1.,-2.22044604925031E-16,0.));
#12233=DIRECTION('center_axis',(-1.,2.22044604925031E-16,0.));
#12234=DIRECTION('ref_axis',(0.,0.,-1.));
#12235=DIRECTION('center_axis',(-2.22044604925031E-16,-1.,0.));
#12236=DIRECTION('ref_axis',(0.,0.,1.));
#12237=DIRECTION('center_axis',(1.,-2.22044604925031E-16,0.));
#12238=DIRECTION('ref_axis',(2.22044604925031E-16,1.,0.));
#12239=DIRECTION('center_axis',(0.,0.,1.));
#12240=DIRECTION('ref_axis',(-1.,2.22044604925031E-16,0.));
#12241=DIRECTION('center_axis',(2.22044604925031E-16,1.,0.));
#12242=DIRECTION('ref_axis',(-0.707106781186553,1.57009245868379E-16,0.707106781186542));
#12243=DIRECTION('',(2.22044604925031E-16,1.,0.));
#12244=DIRECTION('center_axis',(-1.,2.22044604925031E-16,0.));
#12245=DIRECTION('ref_axis',(1.57009245868377E-16,0.707106781186546,-0.707106781186549));
#12246=DIRECTION('',(1.,-2.22044604925031E-16,0.));
#12247=DIRECTION('',(-1.,2.22044604925031E-16,0.));
#12248=DIRECTION('center_axis',(0.408248290463858,0.816496580927738,0.408248290463844));
#12249=DIRECTION('ref_axis',(0.577350269189642,-0.577350269189607,0.577350269189628));
#12250=DIRECTION('center_axis',(0.,0.,1.));
#12251=DIRECTION('ref_axis',(1.,-2.22044604925031E-16,0.));
#12252=DIRECTION('center_axis',(1.75415237890772E-14,-1.,0.));
#12253=DIRECTION('ref_axis',(0.,0.,1.));
#12254=DIRECTION('center_axis',(1.,-2.22044604925031E-16,0.));
#12255=DIRECTION('ref_axis',(-2.22044604925031E-16,-1.,0.));
#12256=DIRECTION('center_axis',(-0.408248290463858,-0.408248290463858,-0.816496580927731));
#12257=DIRECTION('ref_axis',(0.577350269189626,0.577350269189626,-0.577350269189626));
#12258=DIRECTION('center_axis',(0.,0.,-1.));
#12259=DIRECTION('ref_axis',(1.,-2.22044604925031E-16,0.));
#12260=DIRECTION('center_axis',(2.22044604925031E-16,1.,0.));
#12261=DIRECTION('ref_axis',(0.,0.,-1.));
#12262=DIRECTION('center_axis',(1.,-2.22044604925031E-16,0.));
#12263=DIRECTION('ref_axis',(2.22044604925031E-16,1.,0.));
#12264=DIRECTION('center_axis',(2.22044604925031E-16,1.,0.));
#12265=DIRECTION('ref_axis',(0.707106781186553,-1.57009245868379E-16,-0.707106781186543));
#12266=DIRECTION('',(2.22044604925031E-16,1.,0.));
#12267=DIRECTION('center_axis',(-0.408248290463861,0.816496580927728,0.408248290463861));
#12268=DIRECTION('ref_axis',(-0.577350269189623,-0.577350269189631,0.577350269189623));
#12269=DIRECTION('center_axis',(-2.22044604925031E-16,-1.,-8.88178419700124E-15));
#12270=DIRECTION('ref_axis',(-1.,2.22044604925031E-16,0.));
#12271=DIRECTION('center_axis',(0.,0.,1.));
#12272=DIRECTION('ref_axis',(-2.22044604925031E-16,-1.,0.));
#12273=DIRECTION('center_axis',(-1.,2.22044604925031E-16,0.));
#12274=DIRECTION('ref_axis',(0.,0.,1.));
#12275=DIRECTION('center_axis',(0.,0.,1.));
#12276=DIRECTION('ref_axis',(-0.707106781186554,-0.707106781186541,0.));
#12277=DIRECTION('',(0.,0.,1.));
#12278=DIRECTION('center_axis',(-1.,2.22044604925031E-16,0.));
#12279=DIRECTION('ref_axis',(-1.57009245868377E-16,-0.707106781186544,0.707106781186551));
#12280=DIRECTION('',(1.,-2.22044604925031E-16,0.));
#12281=DIRECTION('',(-1.,2.22044604925031E-16,0.));
#12282=DIRECTION('center_axis',(0.408248290463856,0.81649658092774,0.408248290463842));
#12283=DIRECTION('ref_axis',(-0.577350269189626,0.577350269189626,-0.577350269189626));
#12284=DIRECTION('center_axis',(-1.,2.22044604925031E-16,0.));
#12285=DIRECTION('ref_axis',(0.,0.,-1.));
#12286=DIRECTION('center_axis',(2.22044604925031E-16,1.,1.77635683940025E-14));
#12287=DIRECTION('ref_axis',(-1.,2.22044604925031E-16,0.));
#12288=DIRECTION('center_axis',(-1.,2.22044604925031E-16,0.));
#12289=DIRECTION('ref_axis',(1.57009245868376E-16,0.70710678118654,-0.707106781186555));
#12290=DIRECTION('',(1.,-2.22044604925031E-16,0.));
#12291=DIRECTION('',(-1.,2.22044604925031E-16,0.));
#12292=DIRECTION('center_axis',(-2.22044604925031E-16,-1.,0.));
#12293=DIRECTION('ref_axis',(-0.707106781186553,1.57009245868379E-16,-0.707106781186543));
#12294=DIRECTION('',(-2.22044604925031E-16,-1.,0.));
#12295=DIRECTION('center_axis',(1.,-2.22044604925031E-16,-3.55271367880045E-14));
#12296=DIRECTION('ref_axis',(2.8421709430404E-14,0.,1.));
#12297=DIRECTION('center_axis',(2.49644700930717E-14,-0.707106781186548,
0.707106781186548));
#12298=DIRECTION('ref_axis',(-1.57009245868377E-16,-0.707106781186548,-0.707106781186548));
#12299=DIRECTION('center_axis',(-1.,2.22044604925031E-16,0.));
#12300=DIRECTION('ref_axis',(0.,0.,-1.));
#12301=DIRECTION('center_axis',(-2.22044604925031E-16,-1.,0.));
#12302=DIRECTION('ref_axis',(1.,-2.22044604925031E-16,0.));
#12303=DIRECTION('center_axis',(-0.408248290463851,0.816496580927731,-0.408248290463865));
#12304=DIRECTION('ref_axis',(0.577350269189626,0.577350269189626,0.577350269189626));
#12305=DIRECTION('center_axis',(2.22044604925031E-16,1.,0.));
#12306=DIRECTION('ref_axis',(1.,-2.22044604925031E-16,0.));
#12307=DIRECTION('center_axis',(1.,-2.22044604925031E-16,0.));
#12308=DIRECTION('ref_axis',(0.,0.,1.));
#12309=DIRECTION('center_axis',(0.,0.,1.));
#12310=DIRECTION('ref_axis',(0.707106781186548,0.707106781186547,0.));
#12311=DIRECTION('',(0.,0.,1.));
#12312=DIRECTION('center_axis',(1.,-2.22044604925031E-16,0.));
#12313=DIRECTION('ref_axis',(0.,0.,1.));
#12314=DIRECTION('center_axis',(-2.22044604925031E-16,-1.,0.));
#12315=DIRECTION('ref_axis',(0.,0.,1.));
#12316=DIRECTION('center_axis',(1.,-2.22044604925031E-16,0.));
#12317=DIRECTION('ref_axis',(1.57009245868377E-16,0.707106781186548,0.707106781186548));
#12318=DIRECTION('center_axis',(-1.57009245868379E-16,-0.707106781186554,
0.707106781186541));
#12319=DIRECTION('ref_axis',(-1.,2.22044604925031E-16,0.));
#12320=DIRECTION('center_axis',(-0.408248290463854,0.408248290463854,-0.816496580927736));
#12321=DIRECTION('ref_axis',(-0.577350269189616,0.577350269189645,0.577350269189616));
#12322=DIRECTION('center_axis',(-1.,2.22044604925031E-16,0.));
#12323=DIRECTION('ref_axis',(2.22044604925031E-16,1.,0.));
#12324=DIRECTION('center_axis',(0.,0.,1.));
#12325=DIRECTION('ref_axis',(-1.,2.22044604925031E-16,0.));
#12326=DIRECTION('center_axis',(-1.75415237890772E-14,1.,0.));
#12327=DIRECTION('ref_axis',(0.,0.,1.));
#12328=DIRECTION('center_axis',(0.,0.,1.));
#12329=DIRECTION('ref_axis',(-0.707106781186547,0.707106781186548,0.));
#12330=DIRECTION('center_axis',(0.538877990790914,0.827465426020369,0.157833709270475));
#12331=DIRECTION('ref_axis',(0.794104487760817,-0.561516668266341,0.232587819494483));
#12332=DIRECTION('center_axis',(1.,-2.22044604925031E-16,0.));
#12333=DIRECTION('ref_axis',(-1.57009245868377E-16,-0.707106781186548,-0.707106781186548));
#12334=DIRECTION('center_axis',(-1.57009245868377E-16,-0.707106781186548,
0.707106781186548));
#12335=DIRECTION('ref_axis',(1.,-2.22044604925031E-16,0.));
#12336=DIRECTION('center_axis',(-2.22044604925031E-16,-1.,0.));
#12337=DIRECTION('ref_axis',(0.,0.,1.));
#12338=DIRECTION('center_axis',(1.57009245868377E-16,0.707106781186548,
-0.707106781186548));
#12339=DIRECTION('ref_axis',(0.707106781186553,-0.499999999999996,-0.499999999999996));
#12340=DIRECTION('',(1.57009245868377E-16,0.707106781186548,-0.707106781186548));
#12341=DIRECTION('center_axis',(2.22044604925031E-16,1.,0.));
#12342=DIRECTION('ref_axis',(0.707106781186551,-1.57009245868378E-16,0.707106781186544));
#12343=DIRECTION('',(-2.22044604925031E-16,-1.,0.));
#12344=DIRECTION('center_axis',(-0.53887799079092,0.827465426020364,0.157833709270477));
#12345=DIRECTION('ref_axis',(-0.794104487760823,-0.561516668266338,0.23258781949447));
#12346=DIRECTION('center_axis',(-1.57009245868377E-16,-0.707106781186548,
0.707106781186548));
#12347=DIRECTION('ref_axis',(-1.57009245868377E-16,-0.707106781186548,-0.707106781186548));
#12348=DIRECTION('center_axis',(-1.,2.22044604925031E-16,0.));
#12349=DIRECTION('ref_axis',(0.,0.,1.));
#12350=DIRECTION('center_axis',(-2.22044604925031E-16,-1.,0.));
#12351=DIRECTION('ref_axis',(-1.,2.22044604925031E-16,0.));
#12352=DIRECTION('center_axis',(1.,-2.22044604925031E-16,0.));
#12353=DIRECTION('ref_axis',(-2.05142465794791E-16,-0.923879532511288,0.382683432365088));
#12354=DIRECTION('',(-1.,2.22044604925031E-16,0.));
#12355=DIRECTION('',(1.,-2.22044604925031E-16,0.));
#12356=DIRECTION('center_axis',(-2.22044604925031E-16,-1.,0.));
#12357=DIRECTION('ref_axis',(-0.707106781186551,1.57009245868378E-16,0.707106781186544));
#12358=DIRECTION('',(2.22044604925031E-16,1.,0.));
#12359=DIRECTION('center_axis',(-1.57009245868377E-16,-0.707106781186548,
0.707106781186548));
#12360=DIRECTION('ref_axis',(-0.707106781186553,-0.499999999999996,-0.499999999999996));
#12361=DIRECTION('',(-1.57009245868377E-16,-0.707106781186548,0.707106781186548));
#12362=DIRECTION('center_axis',(-1.,2.22044604925031E-16,0.));
#12363=DIRECTION('ref_axis',(1.57009245868375E-16,0.707106781186538,0.707106781186557));
#12364=DIRECTION('',(1.,-2.22044604925031E-16,0.));
#12365=DIRECTION('center_axis',(2.22044604925031E-16,1.,0.));
#12366=DIRECTION('ref_axis',(-0.707106781186551,1.57009245868378E-16,0.707106781186544));
#12367=DIRECTION('',(2.22044604925031E-16,1.,0.));
#12368=DIRECTION('center_axis',(-1.,2.22044604925031E-16,0.));
#12369=DIRECTION('ref_axis',(2.05142465794791E-16,0.923879532511288,-0.382683432365088));
#12370=DIRECTION('',(1.,-2.22044604925031E-16,0.));
#12371=DIRECTION('',(-1.,2.22044604925031E-16,0.));
#12372=DIRECTION('center_axis',(-2.22044604925031E-16,-1.,0.));
#12373=DIRECTION('ref_axis',(0.707106781186551,-1.57009245868378E-16,0.707106781186544));
#12374=DIRECTION('',(-2.22044604925031E-16,-1.,0.));
#12375=DIRECTION('center_axis',(0.,0.,-1.));
#12376=DIRECTION('ref_axis',(0.707106781186547,-0.707106781186548,0.));
#12377=DIRECTION('',(0.,0.,-1.));
#12378=DIRECTION('center_axis',(-2.22044604925031E-16,-1.,0.));
#12379=DIRECTION('ref_axis',(0.707106781186553,-1.57009245868379E-16,0.707106781186542));
#12380=DIRECTION('',(-2.22044604925031E-16,-1.,0.));
#12381=DIRECTION('center_axis',(1.,-2.22044604925031E-16,0.));
#12382=DIRECTION('ref_axis',(-1.57009245868375E-16,-0.707106781186538,0.707106781186557));
#12383=DIRECTION('',(-1.,2.22044604925031E-16,0.));
#12384=DIRECTION('center_axis',(-2.22044604925031E-16,-1.,0.));
#12385=DIRECTION('ref_axis',(-0.707106781186551,1.57009245868378E-16,0.707106781186544));
#12386=DIRECTION('',(2.22044604925031E-16,1.,0.));
#12387=DIRECTION('center_axis',(2.22044604925031E-16,1.,0.));
#12388=DIRECTION('ref_axis',(0.707106781186551,-1.57009245868378E-16,0.707106781186544));
#12389=DIRECTION('',(-2.22044604925031E-16,-1.,0.));
#12390=DIRECTION('center_axis',(0.,0.,1.));
#12391=DIRECTION('ref_axis',(0.707106781186554,0.707106781186541,0.));
#12392=DIRECTION('',(0.,0.,1.));
#12393=DIRECTION('center_axis',(-2.22044604925031E-16,-1.,0.));
#12394=DIRECTION('ref_axis',(0.707106781186551,-1.57009245868378E-16,0.707106781186544));
#12395=DIRECTION('',(-2.22044604925031E-16,-1.,0.));
#12396=DIRECTION('center_axis',(-1.,2.22044604925031E-16,0.));
#12397=DIRECTION('ref_axis',(-1.57009245868375E-16,-0.707106781186538,-0.707106781186557));
#12398=DIRECTION('',(1.,-2.22044604925031E-16,0.));
#12399=DIRECTION('',(-1.,2.22044604925031E-16,0.));
#12400=DIRECTION('center_axis',(0.,0.,1.));
#12401=DIRECTION('ref_axis',(-2.22044604925031E-16,-1.,0.));
#12402=DIRECTION('center_axis',(-2.22044604925031E-16,-1.,0.));
#12403=DIRECTION('ref_axis',(0.,0.,1.));
#12404=DIRECTION('center_axis',(0.,0.,-1.));
#12405=DIRECTION('ref_axis',(-2.22044604925031E-16,-1.,0.));
#12406=DIRECTION('center_axis',(-2.22044604925031E-16,-1.,0.));
#12407=DIRECTION('ref_axis',(0.,0.,1.));
#12408=DIRECTION('center_axis',(0.,0.,-1.));
#12409=DIRECTION('ref_axis',(-2.22044604925031E-16,-1.,0.));
#12410=DIRECTION('center_axis',(2.22044604925031E-16,1.,0.));
#12411=DIRECTION('ref_axis',(0.,0.,-1.));
#12412=DIRECTION('center_axis',(0.,0.,-1.));
#12413=DIRECTION('ref_axis',(-2.22044604925031E-16,-1.,0.));
#12414=DIRECTION('center_axis',(2.22044604925031E-16,1.,0.));
#12415=DIRECTION('ref_axis',(-1.,2.22044604925031E-16,0.));
#12416=DIRECTION('center_axis',(1.57009245868377E-16,0.707106781186548,
0.707106781186548));
#12417=DIRECTION('ref_axis',(1.57009245868377E-16,0.707106781186548,-0.707106781186548));
#12418=DIRECTION('center_axis',(0.,0.,1.));
#12419=DIRECTION('ref_axis',(-2.22044604925031E-16,-1.,0.));
#12420=DIRECTION('center_axis',(0.,0.,1.));
#12421=DIRECTION('ref_axis',(-2.22044604925031E-16,-1.,0.));
#14990=CARTESIAN_POINT('',(0.,0.,0.));
#14991=CARTESIAN_POINT('Origin',(37.3901590350027,65.,45.9189319234316));
#14992=CARTESIAN_POINT('',(33.3901590350027,65.,45.9189319234316));
#14993=CARTESIAN_POINT('Origin',(37.3901590350027,65.,45.9189319234316));
#14994=CARTESIAN_POINT('',(33.3901590350027,49.,45.9189319234316));
#14995=CARTESIAN_POINT('',(33.3901590350027,65.,45.9189319234316));
#14996=CARTESIAN_POINT('Origin',(37.3901590350027,49.,45.9189319234316));
#14997=CARTESIAN_POINT('Origin',(37.3901590350027,49.,45.9189319234316));
#14998=CARTESIAN_POINT('Origin',(-37.3901590350027,65.,45.9189319234316));
#14999=CARTESIAN_POINT('',(-41.3901590350027,65.,45.9189319234316));
#15000=CARTESIAN_POINT('Origin',(-37.3901590350027,65.,45.9189319234316));
#15001=CARTESIAN_POINT('',(-41.3901590350027,49.,45.9189319234316));
#15002=CARTESIAN_POINT('',(-41.3901590350027,65.,45.9189319234316));
#15003=CARTESIAN_POINT('Origin',(-37.3901590350027,49.,45.9189319234316));
#15004=CARTESIAN_POINT('Origin',(-37.3901590350027,49.,45.9189319234316));
#15005=CARTESIAN_POINT('Origin',(-77.3901590350027,65.,45.9189319234316));
#15006=CARTESIAN_POINT('',(-81.3901590350027,65.,45.9189319234316));
#15007=CARTESIAN_POINT('Origin',(-77.3901590350027,65.,45.9189319234316));
#15008=CARTESIAN_POINT('',(-81.3901590350027,49.,45.9189319234316));
#15009=CARTESIAN_POINT('',(-81.3901590350027,65.,45.9189319234316));
#15010=CARTESIAN_POINT('Origin',(-77.3901590350027,49.,45.9189319234316));
#15011=CARTESIAN_POINT('Origin',(-77.3901590350027,49.,45.9189319234316));
#15012=CARTESIAN_POINT('Origin',(77.3901590350027,65.,45.9189319234316));
#15013=CARTESIAN_POINT('',(73.3901590350027,65.,45.9189319234316));
#15014=CARTESIAN_POINT('Origin',(77.3901590350027,65.,45.9189319234316));
#15015=CARTESIAN_POINT('',(73.3901590350027,49.,45.9189319234316));
#15016=CARTESIAN_POINT('',(73.3901590350027,65.,45.9189319234316));
#15017=CARTESIAN_POINT('Origin',(77.3901590350027,49.,45.9189319234316));
#15018=CARTESIAN_POINT('Origin',(77.3901590350027,49.,45.9189319234316));
#15019=CARTESIAN_POINT('Origin',(-37.3901590350027,-65.,45.9189319234316));
#15020=CARTESIAN_POINT('',(-41.3901590350027,-65.,45.9189319234316));
#15021=CARTESIAN_POINT('Origin',(-37.3901590350027,-65.,45.9189319234316));
#15022=CARTESIAN_POINT('',(-41.3901590350027,-49.,45.9189319234316));
#15023=CARTESIAN_POINT('',(-41.3901590350027,-65.,45.9189319234316));
#15024=CARTESIAN_POINT('Origin',(-37.3901590350027,-49.,45.9189319234316));
#15025=CARTESIAN_POINT('Origin',(-37.3901590350027,-49.,45.9189319234316));
#15026=CARTESIAN_POINT('Origin',(77.3901590350027,-65.,45.9189319234316));
#15027=CARTESIAN_POINT('',(73.3901590350027,-65.,45.9189319234316));
#15028=CARTESIAN_POINT('Origin',(77.3901590350027,-65.,45.9189319234316));
#15029=CARTESIAN_POINT('',(73.3901590350027,-49.,45.9189319234316));
#15030=CARTESIAN_POINT('',(73.3901590350027,-65.,45.9189319234316));
#15031=CARTESIAN_POINT('Origin',(77.3901590350027,-49.,45.9189319234316));
#15032=CARTESIAN_POINT('Origin',(77.3901590350027,-49.,45.9189319234316));
#15033=CARTESIAN_POINT('Origin',(-77.3901590350027,-65.,45.9189319234316));
#15034=CARTESIAN_POINT('',(-81.3901590350027,-65.,45.9189319234316));
#15035=CARTESIAN_POINT('Origin',(-77.3901590350027,-65.,45.9189319234316));
#15036=CARTESIAN_POINT('',(-81.3901590350027,-49.,45.9189319234316));
#15037=CARTESIAN_POINT('',(-81.3901590350027,-65.,45.9189319234316));
#15038=CARTESIAN_POINT('Origin',(-77.3901590350027,-49.,45.9189319234316));
#15039=CARTESIAN_POINT('Origin',(-77.3901590350027,-49.,45.9189319234316));
#15040=CARTESIAN_POINT('Origin',(37.3901590350027,-65.,45.9189319234316));
#15041=CARTESIAN_POINT('',(33.3901590350027,-65.,45.9189319234316));
#15042=CARTESIAN_POINT('Origin',(37.3901590350027,-65.,45.9189319234316));
#15043=CARTESIAN_POINT('',(33.3901590350027,-49.,45.9189319234316));
#15044=CARTESIAN_POINT('',(33.3901590350027,-65.,45.9189319234316));
#15045=CARTESIAN_POINT('Origin',(37.3901590350027,-49.,45.9189319234316));
#15046=CARTESIAN_POINT('Origin',(37.3901590350027,-49.,45.9189319234316));
#15047=CARTESIAN_POINT('Origin',(-1.4432899320127E-14,-65.,38.2895355526966));
#15048=CARTESIAN_POINT('',(-90.,-64.5,38.2895355526966));
#15049=CARTESIAN_POINT('',(-89.5,-65.,38.2895355526966));
#15050=CARTESIAN_POINT('Origin',(-89.5,-64.5,38.2895355526966));
#15051=CARTESIAN_POINT('',(-90.,-62.,38.2895355526966));
#15052=CARTESIAN_POINT('',(-90.,1.99840144432528E-14,38.2895355526966));
#15053=CARTESIAN_POINT('',(90.,-62.,38.2895355526966));
#15054=CARTESIAN_POINT('',(-1.37667655053519E-14,-62.,38.2895355526966));
#15055=CARTESIAN_POINT('',(90.,-64.5,38.2895355526966));
#15056=CARTESIAN_POINT('',(90.,-65.,38.2895355526966));
#15057=CARTESIAN_POINT('',(89.5,-65.,38.2895355526966));
#15058=CARTESIAN_POINT('Origin',(89.5,-64.5,38.2895355526966));
#15059=CARTESIAN_POINT('',(-45.,-65.,38.2895355526966));
#15060=CARTESIAN_POINT('Origin',(-1.37667655053519E-14,-62.,34.7895355526966));
#15061=CARTESIAN_POINT('',(-89.5,-65.,34.7895355526966));
#15062=CARTESIAN_POINT('',(-90.,-64.5,34.7895355526966));
#15063=CARTESIAN_POINT('Origin',(-89.5,-64.5,34.7895355526966));
#15064=CARTESIAN_POINT('',(89.5,-65.,34.7895355526966));
#15065=CARTESIAN_POINT('',(-45.,-65.,34.7895355526966));
#15066=CARTESIAN_POINT('',(90.,-64.5,34.7895355526966));
#15067=CARTESIAN_POINT('Origin',(89.5,-64.5,34.7895355526966));
#15068=CARTESIAN_POINT('',(90.,-62.,34.7895355526966));
#15069=CARTESIAN_POINT('',(90.,-63.5,34.7895355526966));
#15070=CARTESIAN_POINT('',(-90.,-62.,34.7895355526966));
#15071=CARTESIAN_POINT('',(-1.37667655053519E-14,-62.,34.7895355526966));
#15072=CARTESIAN_POINT('',(-90.,1.50000000000002,34.7895355526966));
#15073=CARTESIAN_POINT('Origin',(-1.37667655053519E-14,-62.,38.2895355526966));
#15074=CARTESIAN_POINT('',(90.,-62.,35.1447677763483));
#15075=CARTESIAN_POINT('',(-90.,-62.,35.1447677763483));
#15076=CARTESIAN_POINT('Origin',(-89.5,-64.5,32.));
#15077=CARTESIAN_POINT('',(-90.,-64.5,32.5));
#15078=CARTESIAN_POINT('',(-90.,-64.5,32.));
#15079=CARTESIAN_POINT('',(-89.5,-65.,32.));
#15080=CARTESIAN_POINT('Origin',(-89.5,-64.5,32.5));
#15081=CARTESIAN_POINT('',(-89.5,-65.,32.));
#15082=CARTESIAN_POINT('Origin',(-89.5,-64.5,32.));
#15083=CARTESIAN_POINT('',(-89.5,-65.,51.5));
#15084=CARTESIAN_POINT('',(-89.5,-65.,32.));
#15085=CARTESIAN_POINT('',(-90.,-64.5,51.5));
#15086=CARTESIAN_POINT('Origin',(-89.5,-64.5,51.5));
#15087=CARTESIAN_POINT('',(-90.,-64.5,32.));
#15088=CARTESIAN_POINT('Origin',(-90.,-65.,32.));
#15089=CARTESIAN_POINT('',(89.5,-65.,32.));
#15090=CARTESIAN_POINT('',(-90.,-65.,32.));
#15091=CARTESIAN_POINT('',(89.5,-65.,32.));
#15092=CARTESIAN_POINT('Origin',(-90.,-65.,32.));
#15093=CARTESIAN_POINT('',(89.5,-65.,51.5));
#15094=CARTESIAN_POINT('',(89.5,-65.,32.));
#15095=CARTESIAN_POINT('',(-45.,-65.,51.5));
#15096=CARTESIAN_POINT('Origin',(89.5,-64.5,32.));
#15097=CARTESIAN_POINT('',(90.,-64.5,32.5));
#15098=CARTESIAN_POINT('Origin',(89.5,-64.5,32.5));
#15099=CARTESIAN_POINT('',(90.,-64.5,32.));
#15100=CARTESIAN_POINT('Origin',(89.5,-64.5,32.));
#15101=CARTESIAN_POINT('',(90.,-64.5,51.5));
#15102=CARTESIAN_POINT('',(90.,-64.5,32.));
#15103=CARTESIAN_POINT('Origin',(89.5,-64.5,51.5));
#15104=CARTESIAN_POINT('Origin',(90.,-65.,32.));
#15105=CARTESIAN_POINT('',(90.,64.5,32.5));
#15106=CARTESIAN_POINT('',(90.,-32.5,32.5));
#15107=CARTESIAN_POINT('',(90.,64.5,34.7895355526966));
#15108=CARTESIAN_POINT('',(90.,64.5,32.));
#15109=CARTESIAN_POINT('',(90.,62.,34.7895355526966));
#15110=CARTESIAN_POINT('',(90.,-1.50000000000002,34.7895355526966));
#15111=CARTESIAN_POINT('',(90.,62.,38.2895355526966));
#15112=CARTESIAN_POINT('',(90.,62.,35.1447677763483));
#15113=CARTESIAN_POINT('',(90.,64.5,38.2895355526966));
#15114=CARTESIAN_POINT('',(90.,-1.99840144432528E-14,38.2895355526966));
#15115=CARTESIAN_POINT('',(90.,64.5,51.5));
#15116=CARTESIAN_POINT('',(90.,64.5,32.));
#15117=CARTESIAN_POINT('',(90.,23.0395928638606,51.5));
#15118=CARTESIAN_POINT('',(90.,-32.5,51.5));
#15119=CARTESIAN_POINT('',(90.,25.6346603396366,48.904932524224));
#15120=CARTESIAN_POINT('',(90.,5.4779179525988,69.0616749112618));
#15121=CARTESIAN_POINT('',(90.,24.92755355845,47.1978257430375));
#15122=CARTESIAN_POINT('Origin',(90.,24.92755355845,48.1978257430375));
#15123=CARTESIAN_POINT('',(90.,19.545300072509,47.1978257430375));
#15124=CARTESIAN_POINT('',(90.,-19.4326698301817,47.1978257430375));
#15125=CARTESIAN_POINT('',(90.,19.545300072509,36.1978257430375));
#15126=CARTESIAN_POINT('',(90.,19.545300072509,39.8489128715187));
#15127=CARTESIAN_POINT('',(90.,18.545300072509,35.1978257430375));
#15128=CARTESIAN_POINT('Origin',(90.,18.545300072509,36.1978257430375));
#15129=CARTESIAN_POINT('',(90.,-21.0741207385024,35.1978257430375));
#15130=CARTESIAN_POINT('',(90.,-22.9773499637455,35.1978257430375));
#15131=CARTESIAN_POINT('',(90.,-22.0741207385024,36.1978257430375));
#15132=CARTESIAN_POINT('Origin',(90.,-21.0741207385024,36.1978257430375));
#15133=CARTESIAN_POINT('',(90.,-22.0741207385024,47.1978257430375));
#15134=CARTESIAN_POINT('',(90.,-22.0741207385024,33.8489128715187));
#15135=CARTESIAN_POINT('',(90.,-44.3272645584125,47.1978257430375));
#15136=CARTESIAN_POINT('',(90.,-43.2870603692512,47.1978257430375));
#15137=CARTESIAN_POINT('',(90.,-45.3272645584125,48.1978257430375));
#15138=CARTESIAN_POINT('Origin',(90.,-44.3272645584125,48.1978257430375));
#15139=CARTESIAN_POINT('',(90.,-45.3272645584125,51.5));
#15140=CARTESIAN_POINT('',(90.,-45.3272645584125,39.8489128715187));
#15141=CARTESIAN_POINT('',(90.,-32.5,51.5));
#15142=CARTESIAN_POINT('Origin',(1.4432899320127E-14,65.,38.2895355526966));
#15143=CARTESIAN_POINT('',(89.5,65.,38.2895355526966));
#15144=CARTESIAN_POINT('Origin',(89.5,64.5,38.2895355526966));
#15145=CARTESIAN_POINT('',(-90.,62.,38.2895355526966));
#15146=CARTESIAN_POINT('',(1.37667655053519E-14,62.,38.2895355526966));
#15147=CARTESIAN_POINT('',(-90.,64.5,38.2895355526966));
#15148=CARTESIAN_POINT('',(-90.,65.,38.2895355526966));
#15149=CARTESIAN_POINT('',(-89.5,65.,38.2895355526966));
#15150=CARTESIAN_POINT('Origin',(-89.5,64.5,38.2895355526966));
#15151=CARTESIAN_POINT('',(45.,65.,38.2895355526966));
#15152=CARTESIAN_POINT('Origin',(1.37667655053519E-14,62.,34.7895355526966));
#15153=CARTESIAN_POINT('',(89.5,65.,34.7895355526966));
#15154=CARTESIAN_POINT('Origin',(89.5,64.5,34.7895355526966));
#15155=CARTESIAN_POINT('',(-89.5,65.,34.7895355526966));
#15156=CARTESIAN_POINT('',(45.,65.,34.7895355526966));
#15157=CARTESIAN_POINT('',(-90.,64.5,34.7895355526966));
#15158=CARTESIAN_POINT('Origin',(-89.5,64.5,34.7895355526966));
#15159=CARTESIAN_POINT('',(-90.,62.,34.7895355526966));
#15160=CARTESIAN_POINT('',(-90.,63.5,34.7895355526966));
#15161=CARTESIAN_POINT('',(1.37667655053519E-14,62.,34.7895355526966));
#15162=CARTESIAN_POINT('Origin',(1.37667655053519E-14,62.,38.2895355526966));
#15163=CARTESIAN_POINT('',(-90.,62.,35.1447677763483));
#15164=CARTESIAN_POINT('Origin',(89.5,64.5,32.));
#15165=CARTESIAN_POINT('',(89.5,65.,51.5));
#15166=CARTESIAN_POINT('',(89.5,65.,32.));
#15167=CARTESIAN_POINT('Origin',(89.5,64.5,51.5));
#15168=CARTESIAN_POINT('Origin',(-90.,65.,32.));
#15169=CARTESIAN_POINT('',(-90.,-45.3272645584124,51.5));
#15170=CARTESIAN_POINT('',(-90.,32.5,51.5));
#15171=CARTESIAN_POINT('',(-90.,-45.3272645584124,48.1978257430375));
#15172=CARTESIAN_POINT('',(-90.,-45.3272645584124,39.8489128715187));
#15173=CARTESIAN_POINT('',(-90.,-44.3272645584124,47.1978257430375));
#15174=CARTESIAN_POINT('Origin',(-90.,-44.3272645584124,48.1978257430375));
#15175=CARTESIAN_POINT('',(-90.,-22.0741207385023,47.1978257430375));
#15176=CARTESIAN_POINT('',(-90.,21.7129396307488,47.1978257430375));
#15177=CARTESIAN_POINT('',(-90.,-22.0741207385023,36.1978257430375));
#15178=CARTESIAN_POINT('',(-90.,-22.0741207385023,33.8489128715187));
#15179=CARTESIAN_POINT('',(-90.,-21.0741207385023,35.1978257430375));
#15180=CARTESIAN_POINT('Origin',(-90.,-21.0741207385023,36.1978257430375));
#15181=CARTESIAN_POINT('',(-90.,18.5453000725091,35.1978257430375));
#15182=CARTESIAN_POINT('',(-90.,42.0226500362545,35.1978257430375));
#15183=CARTESIAN_POINT('',(-90.,19.5453000725091,36.1978257430375));
#15184=CARTESIAN_POINT('Origin',(-90.,18.5453000725091,36.1978257430375));
#15185=CARTESIAN_POINT('',(-90.,19.5453000725091,47.1978257430375));
#15186=CARTESIAN_POINT('',(-90.,19.5453000725091,39.8489128715187));
#15187=CARTESIAN_POINT('',(-90.,24.9275535584501,47.1978257430375));
#15188=CARTESIAN_POINT('',(-90.,45.5673301698183,47.1978257430375));
#15189=CARTESIAN_POINT('',(-90.,25.6346603396366,48.904932524224));
#15190=CARTESIAN_POINT('Origin',(-90.,24.9275535584501,48.1978257430375));
#15191=CARTESIAN_POINT('',(-90.,23.0395928638606,51.5));
#15192=CARTESIAN_POINT('',(-90.,37.9779179525988,36.5616749112618));
#15193=CARTESIAN_POINT('',(-90.,64.5,51.5));
#15194=CARTESIAN_POINT('',(-90.,32.5,51.5));
#15195=CARTESIAN_POINT('',(-90.,64.5,32.));
#15196=CARTESIAN_POINT('',(-90.,64.5,32.5));
#15197=CARTESIAN_POINT('',(-90.,64.5,32.));
#15198=CARTESIAN_POINT('',(-90.,32.5,32.5));
#15199=CARTESIAN_POINT('Origin',(90.,65.,32.));
#15200=CARTESIAN_POINT('',(-89.5,65.,51.5));
#15201=CARTESIAN_POINT('',(-89.5,65.,32.));
#15202=CARTESIAN_POINT('',(45.,65.,51.5));
#15203=CARTESIAN_POINT('Origin',(-89.5,64.5,32.));
#15204=CARTESIAN_POINT('',(-89.5,65.,32.5));
#15205=CARTESIAN_POINT('',(-89.5,65.,32.));
#15206=CARTESIAN_POINT('Origin',(-89.5,64.5,32.5));
#15207=CARTESIAN_POINT('Origin',(89.5,-44.3272645584125,48.1978257430375));
#15208=CARTESIAN_POINT('',(89.5,-44.3272645584125,47.6978257430375));
#15209=CARTESIAN_POINT('Origin',(89.5,-44.3272645584125,47.1978257430375));
#15210=CARTESIAN_POINT('',(89.5,-44.8272645584125,48.1978257430375));
#15211=CARTESIAN_POINT('Origin',(89.5,-44.3272645584125,48.1978257430375));
#15212=CARTESIAN_POINT('Origin',(89.5,-45.3272645584125,48.1978257430375));
#15213=CARTESIAN_POINT('Origin',(-89.5,-44.3272645584124,48.1978257430375));
#15214=CARTESIAN_POINT('',(-89.5,-44.8272645584124,48.1978257430375));
#15215=CARTESIAN_POINT('Origin',(-89.5,-45.3272645584124,48.1978257430375));
#15216=CARTESIAN_POINT('',(-89.5,-44.3272645584124,47.6978257430375));
#15217=CARTESIAN_POINT('Origin',(-89.5,-44.3272645584124,48.1978257430375));
#15218=CARTESIAN_POINT('Origin',(-89.5,-44.3272645584124,47.1978257430375));
#15219=CARTESIAN_POINT('Origin',(89.5,-22.0741207385024,47.1978257430375));
#15220=CARTESIAN_POINT('',(89.5,-22.0741207385024,47.6978257430375));
#15221=CARTESIAN_POINT('Origin',(89.5,-22.0741207385024,47.1978257430375));
#15222=CARTESIAN_POINT('',(89.5,-21.5741207385024,47.1978257430375));
#15223=CARTESIAN_POINT('Origin',(89.5,-22.0741207385024,47.1978257430375));
#15224=CARTESIAN_POINT('Origin',(89.5,-22.0741207385024,47.1978257430375));
#15225=CARTESIAN_POINT('Origin',(89.5,-45.3272645584125,51.5));
#15226=CARTESIAN_POINT('',(89.5,-45.3272645584125,52.));
#15227=CARTESIAN_POINT('Origin',(89.5,-45.3272645584125,51.5));
#15228=CARTESIAN_POINT('',(89.5,-44.8272645584125,51.5));
#15229=CARTESIAN_POINT('Origin',(89.5,-45.3272645584125,51.5));
#15230=CARTESIAN_POINT('Origin',(89.5,-45.3272645584125,51.5));
#15231=CARTESIAN_POINT('Origin',(89.5,-45.3272645584125,39.8489128715187));
#15232=CARTESIAN_POINT('',(89.5,-44.8272645584125,39.8489128715187));
#15233=CARTESIAN_POINT('Origin',(-89.5,-22.0741207385023,47.1978257430375));
#15234=CARTESIAN_POINT('',(-89.5,-21.5741207385023,47.1978257430375));
#15235=CARTESIAN_POINT('Origin',(-89.5,-22.0741207385023,47.1978257430375));
#15236=CARTESIAN_POINT('',(-89.5,-22.0741207385023,47.6978257430375));
#15237=CARTESIAN_POINT('Origin',(-89.5,-22.0741207385023,47.1978257430375));
#15238=CARTESIAN_POINT('Origin',(-89.5,-22.0741207385023,47.1978257430375));
#15239=CARTESIAN_POINT('Origin',(-89.5,21.7129396307488,47.1978257430375));
#15240=CARTESIAN_POINT('',(-89.5,21.7129396307488,47.6978257430375));
#15241=CARTESIAN_POINT('Origin',(-90.,-22.0741207385023,47.1978257430375));
#15242=CARTESIAN_POINT('',(-90.,-22.0741207385023,47.6978257430375));
#15243=CARTESIAN_POINT('',(-90.,-21.5741207385023,47.1978257430375));
#15244=CARTESIAN_POINT('Origin',(-89.5,-45.3272645584124,51.5));
#15245=CARTESIAN_POINT('',(-89.5,-45.3272645584124,52.));
#15246=CARTESIAN_POINT('Origin',(-89.5,-45.3272645584124,51.5));
#15247=CARTESIAN_POINT('',(-89.5,-44.8272645584124,51.5));
#15248=CARTESIAN_POINT('Origin',(-89.5,-45.3272645584124,51.5));
#15249=CARTESIAN_POINT('Origin',(-89.5,-45.3272645584124,51.5));
#15250=CARTESIAN_POINT('Origin',(-45.,-45.3272645584124,51.5));
#15251=CARTESIAN_POINT('',(-45.,-45.3272645584124,52.));
#15252=CARTESIAN_POINT('',(-45.,-44.8272645584124,51.5));
#15253=CARTESIAN_POINT('Origin',(-89.5,-45.3272645584124,39.8489128715187));
#15254=CARTESIAN_POINT('',(-89.5,-44.8272645584124,39.8489128715187));
#15255=CARTESIAN_POINT('Origin',(89.5,-21.0741207385024,36.1978257430375));
#15256=CARTESIAN_POINT('',(89.5,-21.0741207385024,35.6978257430375));
#15257=CARTESIAN_POINT('Origin',(89.5,-21.0741207385024,35.1978257430375));
#15258=CARTESIAN_POINT('',(89.5,-21.5741207385024,36.1978257430375));
#15259=CARTESIAN_POINT('Origin',(89.5,-21.0741207385024,36.1978257430375));
#15260=CARTESIAN_POINT('Origin',(89.5,-22.0741207385024,36.1978257430375));
#15261=CARTESIAN_POINT('Origin',(89.5,-64.5,51.5));
#15262=CARTESIAN_POINT('',(89.5,-64.5,52.));
#15263=CARTESIAN_POINT('Origin',(89.5,-64.5,51.5));
#15264=CARTESIAN_POINT('Origin',(89.5,-64.5,51.5));
#15265=CARTESIAN_POINT('Origin',(-89.5,-21.0741207385023,36.1978257430375));
#15266=CARTESIAN_POINT('',(-89.5,-21.5741207385023,36.1978257430375));
#15267=CARTESIAN_POINT('Origin',(-89.5,-22.0741207385023,36.1978257430375));
#15268=CARTESIAN_POINT('',(-89.5,-21.0741207385023,35.6978257430375));
#15269=CARTESIAN_POINT('Origin',(-89.5,-21.0741207385023,36.1978257430375));
#15270=CARTESIAN_POINT('Origin',(-89.5,-21.0741207385023,35.1978257430375));
#15271=CARTESIAN_POINT('Origin',(-89.5,-22.0741207385023,33.8489128715187));
#15272=CARTESIAN_POINT('',(-89.5,-21.5741207385023,33.8489128715187));
#15273=CARTESIAN_POINT('Origin',(-90.,-21.0741207385023,36.1978257430375));
#15274=CARTESIAN_POINT('',(-90.,-21.5741207385023,36.1978257430375));
#15275=CARTESIAN_POINT('',(-90.,-21.0741207385023,35.6978257430375));
#15276=CARTESIAN_POINT('Origin',(-89.5,-64.5,51.5));
#15277=CARTESIAN_POINT('',(-89.5,-64.5,52.));
#15278=CARTESIAN_POINT('Origin',(-89.5,-64.5,51.5));
#15279=CARTESIAN_POINT('Origin',(-89.5,-64.5,51.5));
#15280=CARTESIAN_POINT('Origin',(89.5,18.545300072509,36.1978257430375));
#15281=CARTESIAN_POINT('',(89.5,19.045300072509,36.1978257430375));
#15282=CARTESIAN_POINT('Origin',(89.5,19.545300072509,36.1978257430375));
#15283=CARTESIAN_POINT('',(89.5,18.545300072509,35.6978257430375));
#15284=CARTESIAN_POINT('Origin',(89.5,18.545300072509,36.1978257430375));
#15285=CARTESIAN_POINT('Origin',(89.5,18.545300072509,35.1978257430375));
#15286=CARTESIAN_POINT('Origin',(-89.5,18.5453000725091,36.1978257430375));
#15287=CARTESIAN_POINT('',(-89.5,18.5453000725091,35.6978257430375));
#15288=CARTESIAN_POINT('Origin',(-89.5,18.5453000725091,35.1978257430375));
#15289=CARTESIAN_POINT('',(-89.5,19.0453000725091,36.1978257430375));
#15290=CARTESIAN_POINT('Origin',(-89.5,18.5453000725091,36.1978257430375));
#15291=CARTESIAN_POINT('Origin',(-89.5,19.5453000725091,36.1978257430375));
#15292=CARTESIAN_POINT('Origin',(-89.5,42.0226500362545,35.1978257430375));
#15293=CARTESIAN_POINT('',(-89.5,42.0226500362545,35.6978257430375));
#15294=CARTESIAN_POINT('Origin',(-90.,18.5453000725091,36.1978257430375));
#15295=CARTESIAN_POINT('',(-90.,18.5453000725091,35.6978257430375));
#15296=CARTESIAN_POINT('',(-90.,19.0453000725091,36.1978257430375));
#15297=CARTESIAN_POINT('Origin',(89.5,19.545300072509,47.1978257430375));
#15298=CARTESIAN_POINT('',(89.5,19.045300072509,47.1978257430375));
#15299=CARTESIAN_POINT('Origin',(89.5,19.545300072509,47.1978257430375));
#15300=CARTESIAN_POINT('',(89.5,19.545300072509,47.6978257430375));
#15301=CARTESIAN_POINT('Origin',(89.5,19.545300072509,47.1978257430375));
#15302=CARTESIAN_POINT('Origin',(89.5,19.545300072509,47.1978257430375));
#15303=CARTESIAN_POINT('Origin',(89.5,64.5,32.5));
#15304=CARTESIAN_POINT('',(89.5,65.,32.5));
#15305=CARTESIAN_POINT('Origin',(89.5,64.5,32.5));
#15306=CARTESIAN_POINT('',(89.5,64.5,32.));
#15307=CARTESIAN_POINT('Origin',(89.5,64.5,32.5));
#15308=CARTESIAN_POINT('Origin',(89.5,64.5,32.5));
#15309=CARTESIAN_POINT('Origin',(89.5,-32.5,32.5));
#15310=CARTESIAN_POINT('',(89.5,-32.5,32.));
#15311=CARTESIAN_POINT('Origin',(-89.5,19.5453000725091,47.1978257430375));
#15312=CARTESIAN_POINT('',(-89.5,19.5453000725091,47.6978257430375));
#15313=CARTESIAN_POINT('Origin',(-89.5,19.5453000725091,47.1978257430375));
#15314=CARTESIAN_POINT('',(-89.5,19.0453000725091,47.1978257430375));
#15315=CARTESIAN_POINT('Origin',(-89.5,19.5453000725091,47.1978257430375));
#15316=CARTESIAN_POINT('Origin',(-89.5,19.5453000725091,47.1978257430375));
#15317=CARTESIAN_POINT('Origin',(-89.5,19.5453000725091,39.8489128715187));
#15318=CARTESIAN_POINT('',(-89.5,19.0453000725091,39.8489128715187));
#15319=CARTESIAN_POINT('Origin',(-90.,19.5453000725091,47.1978257430375));
#15320=CARTESIAN_POINT('',(-90.,19.0453000725091,47.1978257430375));
#15321=CARTESIAN_POINT('',(-90.,19.5453000725091,47.6978257430375));
#15322=CARTESIAN_POINT('Origin',(-89.5,64.5,32.5));
#15323=CARTESIAN_POINT('',(-89.5,64.5,32.));
#15324=CARTESIAN_POINT('Origin',(-89.5,64.5,32.5));
#15325=CARTESIAN_POINT('Origin',(-89.5,64.5,32.5));
#15326=CARTESIAN_POINT('Origin',(45.,64.5,32.5));
#15327=CARTESIAN_POINT('',(45.,65.,32.5));
#15328=CARTESIAN_POINT('',(45.,64.5,32.));
#15329=CARTESIAN_POINT('Origin',(-89.5,32.5,32.5));
#15330=CARTESIAN_POINT('',(-89.5,32.5,32.));
#15331=CARTESIAN_POINT('Origin',(89.5,24.92755355845,48.1978257430375));
#15332=CARTESIAN_POINT('',(89.5,25.2811069490433,48.5513791336308));
#15333=CARTESIAN_POINT('Origin',(89.5,25.6346603396366,48.904932524224));
#15334=CARTESIAN_POINT('',(89.5,24.92755355845,47.6978257430375));
#15335=CARTESIAN_POINT('Origin',(89.5,24.92755355845,48.1978257430375));
#15336=CARTESIAN_POINT('Origin',(89.5,24.92755355845,47.1978257430375));
#15337=CARTESIAN_POINT('Origin',(89.5,64.5,51.5));
#15338=CARTESIAN_POINT('',(89.5,64.5,52.));
#15339=CARTESIAN_POINT('Origin',(89.5,64.5,51.5));
#15340=CARTESIAN_POINT('Origin',(89.5,64.5,51.5));
#15341=CARTESIAN_POINT('Origin',(89.5,64.5,32.));
#15342=CARTESIAN_POINT('',(89.5,65.,32.));
#15343=CARTESIAN_POINT('Origin',(-89.5,24.9275535584501,48.1978257430375));
#15344=CARTESIAN_POINT('',(-89.5,24.9275535584501,47.6978257430375));
#15345=CARTESIAN_POINT('Origin',(-89.5,24.9275535584501,47.1978257430375));
#15346=CARTESIAN_POINT('',(-89.5,25.2811069490433,48.5513791336308));
#15347=CARTESIAN_POINT('Origin',(-89.5,24.9275535584501,48.1978257430375));
#15348=CARTESIAN_POINT('Origin',(-89.5,25.6346603396366,48.904932524224));
#15349=CARTESIAN_POINT('Origin',(-89.5,64.5,51.5));
#15350=CARTESIAN_POINT('',(-89.5,64.5,52.));
#15351=CARTESIAN_POINT('Origin',(-89.5,64.5,51.5));
#15352=CARTESIAN_POINT('Origin',(-89.5,64.5,51.5));
#15353=CARTESIAN_POINT('Origin',(-89.5,64.5,51.5));
#15354=CARTESIAN_POINT('Origin',(-89.5,64.5,32.));
#15355=CARTESIAN_POINT('Origin',(89.5,23.0395928638606,51.5));
#15356=CARTESIAN_POINT('',(89.5,22.6860394732673,51.1464466094067));
#15357=CARTESIAN_POINT('',(89.5,23.0395928638606,52.));
#15358=CARTESIAN_POINT('Origin',(89.5,23.0395928638606,51.5));
#15359=CARTESIAN_POINT('Origin',(89.5,23.0395928638606,51.5));
#15360=CARTESIAN_POINT('Origin',(89.5,23.0395928638606,51.5));
#15361=CARTESIAN_POINT('Origin',(89.5,5.4779179525988,69.0616749112618));
#15362=CARTESIAN_POINT('',(89.5,5.12436456200553,68.7081215206685));
#15363=CARTESIAN_POINT('Origin',(89.5,-32.5,51.5));
#15364=CARTESIAN_POINT('',(89.5,-32.5,52.));
#15365=CARTESIAN_POINT('Origin',(-89.5,23.0395928638606,51.5));
#15366=CARTESIAN_POINT('',(-89.5,22.6860394732674,51.1464466094067));
#15367=CARTESIAN_POINT('Origin',(-89.5,23.0395928638606,51.5));
#15368=CARTESIAN_POINT('',(-89.5,23.0395928638606,52.));
#15369=CARTESIAN_POINT('Origin',(-89.5,23.0395928638606,51.5));
#15370=CARTESIAN_POINT('Origin',(-89.5,23.0395928638606,51.5));
#15371=CARTESIAN_POINT('Origin',(-45.,23.0395928638606,51.5));
#15372=CARTESIAN_POINT('',(-45.,23.0395928638606,52.));
#15373=CARTESIAN_POINT('',(-45.,22.6860394732673,51.1464466094067));
#15374=CARTESIAN_POINT('Origin',(-89.5,32.5,51.5));
#15375=CARTESIAN_POINT('',(-89.5,32.5,52.));
#15376=CARTESIAN_POINT('Origin',(-89.5,37.9779179525988,36.5616749112618));
#15377=CARTESIAN_POINT('',(-89.5,37.6243645620056,36.2081215206685));
#15378=CARTESIAN_POINT('Origin',(45.,64.5,51.5));
#15379=CARTESIAN_POINT('',(45.,64.5,52.));
#15380=CARTESIAN_POINT('Origin',(-89.5,45.5673301698183,47.1978257430375));
#15381=CARTESIAN_POINT('',(-89.5,45.5673301698183,47.6978257430375));
#15382=CARTESIAN_POINT('Origin',(-90.,24.9275535584501,48.1978257430375));
#15383=CARTESIAN_POINT('',(-90.,24.9275535584501,47.6978257430375));
#15384=CARTESIAN_POINT('',(-90.,25.2811069490433,48.5513791336308));
#15385=CARTESIAN_POINT('Origin',(89.5,-19.4326698301817,47.1978257430375));
#15386=CARTESIAN_POINT('',(89.5,-19.4326698301817,47.6978257430375));
#15387=CARTESIAN_POINT('Origin',(89.5,19.545300072509,39.8489128715187));
#15388=CARTESIAN_POINT('',(89.5,19.045300072509,39.8489128715187));
#15389=CARTESIAN_POINT('Origin',(89.5,-22.9773499637455,35.1978257430375));
#15390=CARTESIAN_POINT('',(89.5,-22.9773499637455,35.6978257430375));
#15391=CARTESIAN_POINT('Origin',(-45.,-64.5,51.5));
#15392=CARTESIAN_POINT('',(-45.,-64.5,52.));
#15393=CARTESIAN_POINT('Origin',(-89.5,32.5,51.5));
#15394=CARTESIAN_POINT('',(-89.5,32.5,52.));
#15395=CARTESIAN_POINT('Origin',(89.5,-32.5,51.5));
#15396=CARTESIAN_POINT('',(89.5,-32.5,52.));
#15397=CARTESIAN_POINT('Origin',(89.5,-22.0741207385024,33.8489128715187));
#15398=CARTESIAN_POINT('',(89.5,-21.5741207385024,33.8489128715187));
#15399=CARTESIAN_POINT('Origin',(89.5,-43.2870603692512,47.1978257430375));
#15400=CARTESIAN_POINT('',(89.5,-43.2870603692512,47.6978257430375));
#15401=CARTESIAN_POINT('Origin',(-90.,-44.3272645584124,48.1978257430375));
#15402=CARTESIAN_POINT('',(-90.,-44.8272645584124,48.1978257430375));
#15403=CARTESIAN_POINT('',(-90.,-44.3272645584124,47.6978257430375));
#15404=CARTESIAN_POINT('Origin',(0.,0.,32.));
#15405=CARTESIAN_POINT('Origin',(-90.,-44.8272645584124,47.6978257430375));
#15406=CARTESIAN_POINT('Origin',(-90.,-21.5741207385023,47.6978257430375));
#15407=CARTESIAN_POINT('Origin',(-90.,-21.5741207385023,35.6978257430375));
#15408=CARTESIAN_POINT('Origin',(-90.,19.0453000725091,35.6978257430375));
#15409=CARTESIAN_POINT('Origin',(-90.,19.0453000725091,47.6978257430375));
#15410=CARTESIAN_POINT('Origin',(-90.,26.1346603396366,47.6978257430375));
#15411=CARTESIAN_POINT('Origin',(90.,65.,32.));
#15412=CARTESIAN_POINT('Origin',(-90.,21.8324860826741,52.));
#15413=CARTESIAN_POINT('Origin',(0.,0.,52.));
#15414=CARTESIAN_POINT('Origin',(0.,0.,52.));
#17817=UNCERTAINTY_MEASURE_WITH_UNIT(LENGTH_MEASURE(0.01),#17837,
'DISTANCE_ACCURACY_VALUE',
'Maximum model space distance between geometric entities at asserted c
onnectivities');
#17824=UNCERTAINTY_MEASURE_WITH_UNIT(LENGTH_MEASURE(0.01),#17837,
'DISTANCE_ACCURACY_VALUE',
'Maximum model space distance between geometric entities at asserted c
onnectivities');
#17829=(
GEOMETRIC_REPRESENTATION_CONTEXT(3)
GLOBAL_UNCERTAINTY_ASSIGNED_CONTEXT((#17817))
GLOBAL_UNIT_ASSIGNED_CONTEXT((#17837,#17839,#17840))
REPRESENTATION_CONTEXT('','3D')
);
#17836=(
GEOMETRIC_REPRESENTATION_CONTEXT(3)
GLOBAL_UNCERTAINTY_ASSIGNED_CONTEXT((#17824))
GLOBAL_UNIT_ASSIGNED_CONTEXT((#17837,#17839,#17840))
REPRESENTATION_CONTEXT('','3D')
);
#17837=(
LENGTH_UNIT()
NAMED_UNIT(*)
SI_UNIT(.MILLI.,.METRE.)
);
#17839=(
NAMED_UNIT(*)
PLANE_ANGLE_UNIT()
SI_UNIT($,.RADIAN.)
);
#17840=(
NAMED_UNIT(*)
SI_UNIT($,.STERADIAN.)
SOLID_ANGLE_UNIT()
);
#17845=SHAPE_DEFINITION_REPRESENTATION(#17856,#17877);
#17856=PRODUCT_DEFINITION_SHAPE('',$,#17889);
#17877=SHAPE_REPRESENTATION('',(#10101),#17829);
#17884=PRODUCT_DEFINITION_CONTEXT('part definition',#17919,'design');
#17889=PRODUCT_DEFINITION('Top_Plate','Top_Plate',#17900,#17884);
#17900=PRODUCT_DEFINITION_FORMATION('',$,#17925);
#17919=APPLICATION_CONTEXT(
'Core Data for Automotive Mechanical Design Process');
#17920=PRODUCT_CONTEXT('part definition',#17919,'mechanical');
#17925=PRODUCT('Top_Plate','Top_Plate',$,(#17920));
#17953=COLOUR_RGB('Light Blue',0.38,0.62,0.78);
#17954=FILL_AREA_STYLE_COLOUR('',#17953);
#17955=FILL_AREA_STYLE('',(#17954));
#17956=SURFACE_STYLE_FILL_AREA(#17955);
#17957=SURFACE_SIDE_STYLE('',(#17956));
#17958=SURFACE_STYLE_USAGE(.BOTH.,#17957);
#17959=PRESENTATION_STYLE_ASSIGNMENT((#17958));
ENDSEC;
END-ISO-10303-21;
